ISO-10303-21;
HEADER;
FILE_DESCRIPTION (('STEP AP214'),
    '1' );
FILE_NAME ('Sliding Jaws.step',
    '2026-10-09T17:48:21',
    ( '' ),
    ( '' ),
    'SwSTEP 2.0',
    'SolidWorks 2024',
    '' );
FILE_SCHEMA (( 'AUTOMOTIVE_DESIGN' ));
ENDSEC;

DATA;
#4=EDGE_CURVE ( 'NONE', #455, #7951, #9514, .T. ) ;
#10=LINE ( 'NONE', #10400, #4062 ) ;
#18=ADVANCED_FACE ( 'NONE', ( #1298 ), #7443, .F. ) ;
#20=ORIENTED_EDGE ( 'NONE', *, *, #14135, .F. ) ;
#22=EDGE_CURVE ( 'NONE', #5823, #14725, #14225, .T. ) ;
#39=ADVANCED_FACE ( 'NONE', ( #3550 ), #5980, .T. ) ;
#48=LINE ( 'NONE', #15323, #3608 ) ;
#50=CARTESIAN_POINT ( 'NONE',  ( 1.634139617129772404, -12.00000029085424025, -0.3335879563140197179 ) ) ;
#55=CARTESIAN_POINT ( 'NONE',  ( -22.96690797774568082, 1.660051434983101380E-15, 52.36213013816526285 ) ) ;
#60=VECTOR ( 'NONE', #13397, 1000.000000000000000 ) ;
#69=ORIENTED_EDGE ( 'NONE', *, *, #2752, .F. ) ;
#70=AXIS2_PLACEMENT_3D ( 'NONE', #89, #11892, #6017 ) ;
#89=CARTESIAN_POINT ( 'NONE',  ( 23.77513017582411692, -1.718469852516944459E-15, 56.45152858669899132 ) ) ;
#91=EDGE_LOOP ( 'NONE', ( #13026, #11376, #12527, #2577 ) ) ;
#100=DIRECTION ( 'NONE',  ( 0.000000000000000000, -1.445602896647339508E-15, -1.000000000000000000 ) ) ;
#101=AXIS2_PLACEMENT_3D ( 'NONE', #55, #7289, #9436 ) ;
#104=AXIS2_PLACEMENT_3D ( 'NONE', #9818, #12003, #8653 ) ;
#120=LINE ( 'NONE', #3929, #1107 ) ;
#127=EDGE_LOOP ( 'NONE', ( #6019, #5479, #5692, #8354 ) ) ;
#134=VERTEX_POINT ( 'NONE', #5029 ) ;
#137=EDGE_CURVE ( 'NONE', #3871, #7132, #3941, .T. ) ;
#138=VECTOR ( 'NONE', #8882, 1000.000000000000000 ) ;
#141=AXIS2_PLACEMENT_3D ( 'NONE', #9942, #7412, #9791 ) ;
#147=CARTESIAN_POINT ( 'NONE',  ( 22.58164641901421632, -12.60000029085423812, -8.183940086454239093 ) ) ;
#151=EDGE_CURVE ( 'NONE', #8289, #4668, #11363, .T. ) ;
#155=ORIENTED_EDGE ( 'NONE', *, *, #10965, .T. ) ;
#159=VECTOR ( 'NONE', #3125, 1000.000000000000000 ) ;
#167=CARTESIAN_POINT ( 'NONE',  ( -13.41835358098578723, 11.39999970914575833, 0.2664120436859911956 ) ) ;
#169=DIRECTION ( 'NONE',  ( -9.035018104045795506E-17, -0.9860132971832696880, -0.1666666666666656860 ) ) ;
#175=DIRECTION ( 'NONE',  ( -0.000000000000000000, 1.000000000000000000, 4.336808689942017736E-16 ) ) ;
#200=DIRECTION ( 'NONE',  ( 0.000000000000000000, 0.1240337885538713436, -0.9922779949676268085 ) ) ;
#205=EDGE_LOOP ( 'NONE', ( #7542, #9169, #8571, #7456 ) ) ;
#223=CARTESIAN_POINT ( 'NONE',  ( 22.58164641901421277, 7.308633194218583817, -28.96834603255778262 ) ) ;
#227=ORIENTED_EDGE ( 'NONE', *, *, #3079, .F. ) ;
#237=CARTESIAN_POINT ( 'NONE',  ( 10.10045295220800554, 10.99999970914572778, 70.08978589960025829 ) ) ;
#241=DIRECTION ( 'NONE',  ( -1.000000000000000000, 0.000000000000000000, 0.000000000000000000 ) ) ;
#257=DIRECTION ( 'NONE',  ( 0.000000000000000000, 0.000000000000000000, -1.000000000000000000 ) ) ;
#268=LINE ( 'NONE', #10989, #10255 ) ;
#285=AXIS2_PLACEMENT_3D ( 'NONE', #3423, #3496, #1409 ) ;
#291=CARTESIAN_POINT ( 'NONE',  ( -12.81835358098578759, -12.00000029085424202, -0.3335879563140091153 ) ) ;
#292=EDGE_CURVE ( 'NONE', #3454, #15328, #4849, .T. ) ;
#296=ADVANCED_FACE ( 'NONE', ( #6886 ), #12771, .T. ) ;
#302=AXIS2_PLACEMENT_3D ( 'NONE', #4626, #14004, #968 ) ;
#305=VECTOR ( 'NONE', #8128, 1000.000000000000000 ) ;
#321=AXIS2_PLACEMENT_3D ( 'NONE', #2492, #3670, #13142 ) ;
#324=UNCERTAINTY_MEASURE_WITH_UNIT (LENGTH_MEASURE( 1.000000000000000082E-05 ), #9126, 'distance_accuracy_value', 'NONE');
#327=AXIS2_PLACEMENT_3D ( 'NONE', #4537, #4852, #6031 ) ;
#329=CIRCLE ( 'NONE', #7787, 0.5999999999999999778 ) ;
#332=CARTESIAN_POINT ( 'NONE',  ( 22.58164641901421632, 11.99999970914576330, -14.13358795631400611 ) ) ;
#333=DIRECTION ( 'NONE',  ( 0.000000000000000000, 0.000000000000000000, -1.000000000000000000 ) ) ;
#336=( BOUNDED_CURVE ( )  B_SPLINE_CURVE ( 3, ( #13396, #4082, #13474, #8809 ),
 .UNSPECIFIED., .F., .F. ) 
 B_SPLINE_CURVE_WITH_KNOTS ( ( 4, 4 ),
 ( 1.570796326794896780, 3.141592653589790896 ),
 .UNSPECIFIED. ) 
 CURVE ( )  GEOMETRIC_REPRESENTATION_ITEM ( )  RATIONAL_B_SPLINE_CURVE ( ( 1.000000000000000000, 0.8047378541243654926, 0.8047378541243654926, 1.000000000000000000 ) ) 
 REPRESENTATION_ITEM ( '' )  );
#340=DIRECTION ( 'NONE',  ( -1.000000000000000000, -0.000000000000000000, -0.000000000000000000 ) ) ;
#354=DIRECTION ( 'NONE',  ( -0.9961946980917452121, 7.200509705930738460E-17, -0.08715574274766156593 ) ) ;
#364=ORIENTED_EDGE ( 'NONE', *, *, #13152, .F. ) ;
#367=ORIENTED_EDGE ( 'NONE', *, *, #5633, .F. ) ;
#370=ORIENTED_EDGE ( 'NONE', *, *, #5864, .T. ) ;
#371=ORIENTED_EDGE ( 'NONE', *, *, #4615, .F. ) ;
#375=DIRECTION ( 'NONE',  ( 1.000000000000000000, 0.000000000000000000, -0.000000000000000000 ) ) ;
#381=FACE_OUTER_BOUND ( 'NONE', #1875, .T. ) ;
#383=FACE_OUTER_BOUND ( 'NONE', #7346, .T. ) ;
#391=DIRECTION ( 'NONE',  ( 0.000000000000000000, -0.000000000000000000, 1.000000000000000000 ) ) ;
#392=CIRCLE ( 'NONE', #2369, 0.6000000000000000888 ) ;
#402=CIRCLE ( 'NONE', #10057, 0.6000000000000000888 ) ;
#410=ORIENTED_EDGE ( 'NONE', *, *, #13960, .T. ) ;
#411=VERTEX_POINT ( 'NONE', #13239 ) ;
#431=ADVANCED_FACE ( 'NONE', ( #12219 ), #11046, .T. ) ;
#444=CARTESIAN_POINT ( 'NONE',  ( -3.388210470019727971, 7.386374946223608119E-17, -0.2964300057665807953 ) ) ;
#448=EDGE_CURVE ( 'NONE', #11545, #1533, #8802, .T. ) ;
#455=VERTEX_POINT ( 'NONE', #13619 ) ;
#466=CARTESIAN_POINT ( 'NONE',  ( 16.25361217826510085, -12.00000029085424025, -0.2147805754215613983 ) ) ;
#468=ORIENTED_EDGE ( 'NONE', *, *, #7417, .F. ) ;
#480=LINE ( 'NONE', #9928, #2075 ) ;
#494=CYLINDRICAL_SURFACE ( 'NONE', #141, 0.6000000000000000888 ) ;
#497=DIRECTION ( 'NONE',  ( 0.000000000000000000, 1.000000000000000000, 0.000000000000000000 ) ) ;
#504=CARTESIAN_POINT ( 'NONE',  ( 17.18164641901421419, -11.40000029085424238, 0.8664120436859875651 ) ) ;
#513=DIRECTION ( 'NONE',  ( 0.9999934663667180423, -1.567696289299852607E-18, 0.003614861529252313879 ) ) ;
#534=ORIENTED_EDGE ( 'NONE', *, *, #859, .T. ) ;
#536=ORIENTED_EDGE ( 'NONE', *, *, #7075, .T. ) ;
#537=VECTOR ( 'NONE', #14076, 1000.000000000000000 ) ;
#559=CIRCLE ( 'NONE', #10455, 0.5999999999999998668 ) ;
#576=EDGE_CURVE ( 'NONE', #1167, #13856, #4919, .T. ) ;
#584=DIRECTION ( 'NONE',  ( 0.000000000000000000, 0.000000000000000000, -1.000000000000000000 ) ) ;
#591=ORIENTED_EDGE ( 'NONE', *, *, #448, .T. ) ;
#600=( LENGTH_UNIT ( ) NAMED_UNIT ( * ) SI_UNIT ( .MILLI., .METRE. ) );
#601=DIRECTION ( 'NONE',  ( 0.000000000000000000, 0.000000000000000000, -1.000000000000000000 ) ) ;
#606=ORIENTED_EDGE ( 'NONE', *, *, #7544, .T. ) ;
#610=EDGE_CURVE ( 'NONE', #3634, #11545, #14210, .T. ) ;
#648=ORIENTED_EDGE ( 'NONE', *, *, #2337, .F. ) ;
#655=EDGE_LOOP ( 'NONE', ( #1300, #8723, #4606, #8416 ) ) ;
#666=CARTESIAN_POINT ( 'NONE',  ( 21.98164641901421135, -11.40000029085424238, -0.3335879563140091153 ) ) ;
#669=CARTESIAN_POINT ( 'NONE',  ( 17.10018810948620072, -11.27427741823326279, 0.2691656137646578073 ) ) ;
#685=ORIENTED_EDGE ( 'NONE', *, *, #9338, .T. ) ;
#688=ORIENTED_EDGE ( 'NONE', *, *, #13426, .F. ) ;
#697=CARTESIAN_POINT ( 'NONE',  ( 10.10406781373725771, 10.99999970914572778, 69.08979243323354069 ) ) ;
#707=ORIENTED_EDGE ( 'NONE', *, *, #4, .F. ) ;
#709=ORIENTED_EDGE ( 'NONE', *, *, #610, .T. ) ;
#712=DIRECTION ( 'NONE',  ( 0.9961946980917452121, -7.200509705930739692E-17, 0.08715574274766157981 ) ) ;
#737=LINE ( 'NONE', #11142, #6125 ) ;
#746=DIRECTION ( 'NONE',  ( 0.000000000000000000, 4.336808689942017736E-16, -1.000000000000000000 ) ) ;
#752=ORIENTED_EDGE ( 'NONE', *, *, #11402, .T. ) ;
#753=ORIENTED_EDGE ( 'NONE', *, *, #1823, .T. ) ;
#758=AXIS2_PLACEMENT_3D ( 'NONE', #7496, #7418, #6415 ) ;
#776=ORIENTED_EDGE ( 'NONE', *, *, #5824, .T. ) ;
#787=AXIS2_PLACEMENT_3D ( 'NONE', #14350, #6082, #2412 ) ;
#793=ORIENTED_EDGE ( 'NONE', *, *, #9979, .T. ) ;
#798=ORIENTED_EDGE ( 'NONE', *, *, #12472, .T. ) ;
#810=CARTESIAN_POINT ( 'NONE',  ( 21.98164641901421135, -12.50000029085423847, -8.775548064764199907 ) ) ;
#822=AXIS2_PLACEMENT_3D ( 'NONE', #12682, #4233, #2055 ) ;
#829=DIRECTION ( 'NONE',  ( 0.08715574274766167695, 0.000000000000000000, -0.9961946980917453232 ) ) ;
#830=CARTESIAN_POINT ( 'NONE',  ( 22.58164641901421632, 12.59999970914575940, -8.183940086454237317 ) ) ;
#836=EDGE_LOOP ( 'NONE', ( #1705, #12143 ) ) ;
#856=VERTEX_POINT ( 'NONE', #2014 ) ;
#859=EDGE_CURVE ( 'NONE', #2988, #2847, #6988, .T. ) ;
#869=AXIS2_PLACEMENT_3D ( 'NONE', #14614, #1744, #12312 ) ;
#874=ORIENTED_EDGE ( 'NONE', *, *, #9028, .F. ) ;
#876=EDGE_CURVE ( 'NONE', #411, #12032, #15182, .T. ) ;
#881=AXIS2_PLACEMENT_3D ( 'NONE', #3446, #7110, #2276 ) ;
#895=ORIENTED_EDGE ( 'NONE', *, *, #1284, .T. ) ;
#906=PLANE ( 'NONE',  #4282 ) ;
#925=DIRECTION ( 'NONE',  ( -1.000000000000000000, 1.734723475976808672E-15, 0.000000000000000000 ) ) ;
#927=LINE ( 'NONE', #10383, #12346 ) ;
#936=UNCERTAINTY_MEASURE_WITH_UNIT (LENGTH_MEASURE( 1.000000000000000082E-05 ), #9896, 'distance_accuracy_value', 'NONE');
#948=AXIS2_PLACEMENT_3D ( 'NONE', #13719, #7962, #10362 ) ;
#959=VECTOR ( 'NONE', #10043, 1000.000000000000000 ) ;
#968=DIRECTION ( 'NONE',  ( 0.003614861529253208996, 0.000000000000000000, -0.9999934663667179313 ) ) ;
#971=DIRECTION ( 'NONE',  ( 0.000000000000000000, 1.000000000000000000, 0.000000000000000000 ) ) ;
#978=SURFACE_SIDE_STYLE ('',( #15322 ) ) ;
#980=EDGE_CURVE ( 'NONE', #2847, #1167, #402, .T. ) ;
#982=EDGE_CURVE ( 'NONE', #7121, #1333, #12154, .T. ) ;
#999=DIRECTION ( 'NONE',  ( -0.000000000000000000, -1.000000000000000000, -0.000000000000000000 ) ) ;
#1004=ADVANCED_FACE ( 'NONE', ( #8590 ), #11077, .T. ) ;
#1005=ORIENTED_EDGE ( 'NONE', *, *, #9618, .T. ) ;
#1013=DIRECTION ( 'NONE',  ( -0.08715574274766167695, 0.000000000000000000, 0.9961946980917453232 ) ) ;
#1042=CARTESIAN_POINT ( 'NONE',  ( 17.14647606710965988, -3.654413409933304102, 0.2671853888517377595 ) ) ;
#1043=AXIS2_PLACEMENT_3D ( 'NONE', #2565, #10946, #14427 ) ;
#1044=ORIENTED_EDGE ( 'NONE', *, *, #3572, .F. ) ;
#1046=ORIENTED_EDGE ( 'NONE', *, *, #8355, .T. ) ;
#1047=EDGE_CURVE ( 'NONE', #14750, #8289, #1453, .T. ) ;
#1052=DIRECTION ( 'NONE',  ( -0.9961946980917453232, 7.200509705930739692E-17, -0.08715574274766156593 ) ) ;
#1057=AXIS2_PLACEMENT_3D ( 'NONE', #12391, #5489, #1683 ) ;
#1065=CIRCLE ( 'NONE', #9480, 1.199999999999999734 ) ;
#1078=DIRECTION ( 'NONE',  ( 0.000000000000000000, 0.000000000000000000, 1.000000000000000000 ) ) ;
#1080=CARTESIAN_POINT ( 'NONE',  ( 17.16405274069114739, 3.654316742536410256, 0.2664120436859874763 ) ) ;
#1104=CARTESIAN_POINT ( 'NONE',  ( 21.98164641901421135, 11.99999970914576330, -8.733587956314005751 ) ) ;
#1107=VECTOR ( 'NONE', #14384, 1000.000000000000114 ) ;
#1108=ORIENTED_EDGE ( 'NONE', *, *, #8495, .F. ) ;
#1119=FACE_OUTER_BOUND ( 'NONE', #655, .T. ) ;
#1121=DIRECTION ( 'NONE',  ( -7.395386697914957063E-16, -1.000000000000000000, 0.000000000000000000 ) ) ;
#1122=ORIENTED_EDGE ( 'NONE', *, *, #14847, .T. ) ;
#1123=DIRECTION ( 'NONE',  ( 0.000000000000000000, 0.000000000000000000, 1.000000000000000000 ) ) ;
#1127=B_SPLINE_CURVE_WITH_KNOTS ( 'NONE', 3,
 ( #8403, #10724, #13144, #12054, #4922, #3901, #1422, #1569, #2574, #2494 ),
 .UNSPECIFIED., .F., .F.,
 ( 4, 2, 2, 2, 4 ),
 ( 0.000000000000000000, 0.0002904196669106299503, 0.0005808393338212599006, 0.0008712590007318899051, 0.001161678667642519801 ),
 .UNSPECIFIED. ) ;
#1136=AXIS2_PLACEMENT_3D ( 'NONE', #1177, #11811, #1248 ) ;
#1145=ORIENTED_EDGE ( 'NONE', *, *, #13426, .T. ) ;
#1155=CARTESIAN_POINT ( 'NONE',  ( -13.41835358098578723, 11.99999970914575975, 0.2664120436859911956 ) ) ;
#1157=CARTESIAN_POINT ( 'NONE',  ( -4.522482571421199360, 11.99999970914574021, 70.03692566716181034 ) ) ;
#1163=CARTESIAN_POINT ( 'NONE',  ( -4.522482571421199360, -11.58578672848118352, 70.03692566716176771 ) ) ;
#1167=VERTEX_POINT ( 'NONE', #7885 ) ;
#1170=B_SPLINE_CURVE_WITH_KNOTS ( 'NONE', 3,
 ( #4775, #10827, #9570, #7117, #1203, #3612, #8349, #6037, #14311, #8418 ),
 .UNSPECIFIED., .F., .F.,
 ( 4, 2, 2, 2, 4 ),
 ( -1.214224233790302196E-05, 0.0002824113887451626783, 0.0005769650198282283904, 0.0008715186509112941024, 0.001166072281994359923 ),
 .UNSPECIFIED. ) ;
#1176=CARTESIAN_POINT ( 'NONE',  ( -13.41835358098578723, 12.39999970914576188, -9.367156043074160721 ) ) ;
#1177=CARTESIAN_POINT ( 'NONE',  ( -13.41835358098578723, -2.908542394189813650E-07, -11.73358795631400930 ) ) ;
#1180=CARTESIAN_POINT ( 'NONE',  ( 22.58164641901421632, -12.40000029085423883, -9.367156043074160721 ) ) ;
#1192=EDGE_LOOP ( 'NONE', ( #874, #14609, #11340, #2381 ) ) ;
#1196=FACE_OUTER_BOUND ( 'NONE', #11852, .T. ) ;
#1203=CARTESIAN_POINT ( 'NONE',  ( 16.59106891544169571, 11.89170417910964872, 0.2558302058915557509 ) ) ;
#1231=CARTESIAN_POINT ( 'NONE',  ( -9.503456061879928640, -12.00000029085427222, 69.60114695342350899 ) ) ;
#1238=ORIENTED_EDGE ( 'NONE', *, *, #4504, .F. ) ;
#1239=ORIENTED_EDGE ( 'NONE', *, *, #2752, .T. ) ;
#1240=ORIENTED_EDGE ( 'NONE', *, *, #3079, .T. ) ;
#1242=EDGE_CURVE ( 'NONE', #2988, #13856, #2144, .T. ) ;
#1248=DIRECTION ( 'NONE',  ( 0.000000000000000000, 0.000000000000000000, -1.000000000000000000 ) ) ;
#1255=CYLINDRICAL_SURFACE ( 'NONE', #70, 4.000000000000004441 ) ;
#1269=LINE ( 'NONE', #9488, #14702 ) ;
#1273=CIRCLE ( 'NONE', #12437, 2.999999999999999112 ) ;
#1284=EDGE_CURVE ( 'NONE', #14787, #6768, #3295, .T. ) ;
#1297=COLOUR_RGB ( '', 0.09019608, 0.27058824, 0.51372549) ;
#1298=FACE_OUTER_BOUND ( 'NONE', #1404, .T. ) ;
#1300=ORIENTED_EDGE ( 'NONE', *, *, #9712, .F. ) ;
#1302=ORIENTED_EDGE ( 'NONE', *, *, #3096, .T. ) ;
#1303=AXIS2_PLACEMENT_3D ( 'NONE', #4083, #13475, #7432 ) ;
#1310=DIRECTION ( 'NONE',  ( -0.08715574274766053897, 1.511911130105616684E-16, 0.9961946980917454342 ) ) ;
#1319=VECTOR ( 'NONE', #11873, 1000.000000000000000 ) ;
#1327=CARTESIAN_POINT ( 'NONE',  ( -12.81835358098578403, 11.99999970914575798, -0.3335879563140091153 ) ) ;
#1330=CARTESIAN_POINT ( 'NONE',  ( 10.10406781373725771, -11.00000029085427045, 69.08979243323352648 ) ) ;
#1333=VERTEX_POINT ( 'NONE', #2135 ) ;
#1337=ORIENTED_EDGE ( 'NONE', *, *, #9200, .T. ) ;
#1339=CARTESIAN_POINT ( 'NONE',  ( 1.581646419014216542, 11.99999970914575798, -0.3335879563140091153 ) ) ;
#1350=AXIS2_PLACEMENT_3D ( 'NONE', #14641, #7534, #8753 ) ;
#1352=DIRECTION ( 'NONE',  ( 0.000000000000000000, 0.000000000000000000, -1.000000000000000000 ) ) ;
#1358=ORIENTED_EDGE ( 'NONE', *, *, #3640, .T. ) ;
#1361=ORIENTED_EDGE ( 'NONE', *, *, #15071, .T. ) ;
#1374=CARTESIAN_POINT ( 'NONE',  ( 11.02010870769206541, -85.69524470659703752, 70.09311034953161368 ) ) ;
#1385=ORIENTED_EDGE ( 'NONE', *, *, #9354, .T. ) ;
#1395=DIRECTION ( 'NONE',  ( -1.000000000000000000, 0.000000000000000000, -0.000000000000000000 ) ) ;
#1396=CARTESIAN_POINT ( 'NONE',  ( 10.10406781373725948, -11.00000029085427933, 69.08979243323352648 ) ) ;
#1404=EDGE_LOOP ( 'NONE', ( #10933, #10528, #6124, #1385 ) ) ;
#1409=DIRECTION ( 'NONE',  ( 1.000000000000000000, 0.000000000000000000, 0.000000000000000000 ) ) ;
#1417=DIRECTION ( 'NONE',  ( 0.08715574274766176022, 4.320305823558445788E-16, -0.9961946980917453232 ) ) ;
#1422=CARTESIAN_POINT ( 'NONE',  ( 16.50208930436313892, -11.93241838496953910, 0.2532233872428652499 ) ) ;
#1428=CARTESIAN_POINT ( 'NONE',  ( 10.10406781373725771, -11.00000029085428110, 70.08979243323352648 ) ) ;
#1432=LINE ( 'NONE', #3911, #10285 ) ;
#1433=( BOUNDED_CURVE ( )  B_SPLINE_CURVE ( 3, ( #9933, #12277, #5531, #1651 ),
 .UNSPECIFIED., .F., .T. ) 
 B_SPLINE_CURVE_WITH_KNOTS ( ( 4, 4 ),
 ( 4.336808689942018229E-16, 1.570796326794896780 ),
 .UNSPECIFIED. ) 
 CURVE ( )  GEOMETRIC_REPRESENTATION_ITEM ( )  RATIONAL_B_SPLINE_CURVE ( ( 1.000000000000000000, 0.8047378541243650485, 0.8047378541243650485, 1.000000000000000000 ) ) 
 REPRESENTATION_ITEM ( '' )  );
#1436=VECTOR ( 'NONE', #7493, 1000.000000000000000 ) ;
#1453=LINE ( 'NONE', #1525, #15254 ) ;
#1454=DIRECTION ( 'NONE',  ( 0.9961946980917453232, -3.779777825264105188E-17, 0.08715574274766176022 ) ) ;
#1456=ORIENTED_EDGE ( 'NONE', *, *, #11326, .T. ) ;
#1464=ORIENTED_EDGE ( 'NONE', *, *, #3572, .T. ) ;
#1471=ADVANCED_FACE ( 'NONE', ( #2828 ), #14378, .T. ) ;
#1472=DIRECTION ( 'NONE',  ( 0.000000000000000000, 0.000000000000000000, -1.000000000000000000 ) ) ;
#1473=DIRECTION ( 'NONE',  ( 0.000000000000000000, 0.000000000000000000, 1.000000000000000000 ) ) ;
#1475=CYLINDRICAL_SURFACE ( 'NONE', #1350, 2.999999999999999112 ) ;
#1488=LINE ( 'NONE', #2882, #2375 ) ;
#1500=ORIENTED_EDGE ( 'NONE', *, *, #4502, .F. ) ;
#1504=DIRECTION ( 'NONE',  ( 0.000000000000000000, 0.000000000000000000, -1.000000000000000000 ) ) ;
#1507=LINE ( 'NONE', #5083, #2323 ) ;
#1508=DIRECTION ( 'NONE',  ( 0.000000000000000000, 0.000000000000000000, -1.000000000000000000 ) ) ;
#1518=CARTESIAN_POINT ( 'NONE',  ( -4.522482571421199360, 11.99999970914574021, 70.03692566716181034 ) ) ;
#1525=CARTESIAN_POINT ( 'NONE',  ( 17.12895037488186389, -12.00000029085424025, 0.2687305842673423095 ) ) ;
#1533=VERTEX_POINT ( 'NONE', #3056 ) ;
#1548=ORIENTED_EDGE ( 'NONE', *, *, #980, .F. ) ;
#1550=VERTEX_POINT ( 'NONE', #11199 ) ;
#1562=FACE_BOUND ( 'NONE', #6813, .T. ) ;
#1568=ORIENTED_EDGE ( 'NONE', *, *, #8174, .F. ) ;
#1569=CARTESIAN_POINT ( 'NONE',  ( 16.31427926918344085, -11.98694815350135379, 0.2637688259798897095 ) ) ;
#1573=ORIENTED_EDGE ( 'NONE', *, *, #6520, .F. ) ;
#1583=CARTESIAN_POINT ( 'NONE',  ( -13.41835358098578723, 11.99999970914576330, -14.13358795631400611 ) ) ;
#1602=CARTESIAN_POINT ( 'NONE',  ( 17.18164641901421419, -11.40000029085424238, 0.2664120436859911956 ) ) ;
#1605=PLANE ( 'NONE',  #3535 ) ;
#1619=CARTESIAN_POINT ( 'NONE',  ( -12.81835358098578403, -12.00000029085423670, -11.73358795631400930 ) ) ;
#1622=CARTESIAN_POINT ( 'NONE',  ( 21.98164641901421135, 11.39999970914575833, -0.3335879563140091153 ) ) ;
#1625=ORIENTED_EDGE ( 'NONE', *, *, #9039, .T. ) ;
#1627=ORIENTED_EDGE ( 'NONE', *, *, #8184, .F. ) ;
#1644=CARTESIAN_POINT ( 'NONE',  ( -4.435020996998821019, 11.99999970914572778, 69.03723529703218276 ) ) ;
#1649=ORIENTED_EDGE ( 'NONE', *, *, #9028, .T. ) ;
#1651=CARTESIAN_POINT ( 'NONE',  ( -12.81835358098578403, 11.99999970914575798, -0.3335879563140091153 ) ) ;
#1662=EDGE_CURVE ( 'NONE', #15166, #12591, #13571, .T. ) ;
#1680=LINE ( 'NONE', #3854, #7097 ) ;
#1683=DIRECTION ( 'NONE',  ( 0.000000000000000000, 0.000000000000000000, 1.000000000000000000 ) ) ;
#1686=DIRECTION ( 'NONE',  ( 0.9961946980917453232, 0.000000000000000000, 0.08715574274766210716 ) ) ;
#1687=ORIENTED_EDGE ( 'NONE', *, *, #14425, .F. ) ;
#1690=DIRECTION ( 'NONE',  ( 0.9999934663667179313, -1.567696289299852414E-18, 0.003614861529252313445 ) ) ;
#1704=ORIENTED_EDGE ( 'NONE', *, *, #2972, .F. ) ;
#1705=ORIENTED_EDGE ( 'NONE', *, *, #14847, .F. ) ;
#1722=ORIENTED_EDGE ( 'NONE', *, *, #4298, .T. ) ;
#1728=DIRECTION ( 'NONE',  ( 1.000000000000000000, 0.000000000000000000, 0.000000000000000000 ) ) ;
#1731=LINE ( 'NONE', #14763, #1436 ) ;
#1739=PRODUCT ( 'Sliding Jaws', 'Sliding Jaws', '', ( #3689 ) ) ;
#1744=DIRECTION ( 'NONE',  ( 0.9961946980917452121, -3.779777825264104572E-17, 0.08715574274766174634 ) ) ;
#1750=DIRECTION ( 'NONE',  ( 1.000000000000000000, -0.000000000000000000, 0.000000000000000000 ) ) ;
#1752=CARTESIAN_POINT ( 'NONE',  ( -12.81835358098578403, 11.99999970914575975, -8.183940086454237317 ) ) ;
#1754=( NAMED_UNIT ( * ) SI_UNIT ( $, .STERADIAN. ) SOLID_ANGLE_UNIT ( ) );
#1764=CIRCLE ( 'NONE', #3492, 0.6000000000000000888 ) ;
#1767=CARTESIAN_POINT ( 'NONE',  ( -9.503456061879925088, 11.99999970914574021, 69.60114695342350899 ) ) ;
#1768=DIRECTION ( 'NONE',  ( -0.000000000000000000, 1.000000000000000000, 4.336808689942017736E-16 ) ) ;
#1769=DIRECTION ( 'NONE',  ( 0.000000000000000000, 0.000000000000000000, 1.000000000000000000 ) ) ;
#1785=LINE ( 'NONE', #9447, #8840 ) ;
#1797=ORIENTED_EDGE ( 'NONE', *, *, #2706, .F. ) ;
#1798=DIRECTION ( 'NONE',  ( 1.000000000000000000, 0.000000000000000000, 0.000000000000000000 ) ) ;
#1805=ADVANCED_FACE ( 'NONE', ( #6936 ), #11505, .T. ) ;
#1817=VECTOR ( 'NONE', #4025, 1000.000000000000000 ) ;
#1821=EDGE_CURVE ( 'NONE', #6249, #3634, #5632, .T. ) ;
#1823=EDGE_CURVE ( 'NONE', #8050, #4503, #5863, .T. ) ;
#1824=CIRCLE ( 'NONE', #10491, 0.5999999999999999778 ) ;
#1830=( BOUNDED_CURVE ( )  B_SPLINE_CURVE ( 3, ( #7733, #5488, #13923, #9035 ),
 .UNSPECIFIED., .F., .T. ) 
 B_SPLINE_CURVE_WITH_KNOTS ( ( 4, 4 ),
 ( -2.664535259100375697E-15, 1.570796326794896780 ),
 .UNSPECIFIED. ) 
 CURVE ( )  GEOMETRIC_REPRESENTATION_ITEM ( )  RATIONAL_B_SPLINE_CURVE ( ( 1.000000000000000000, 0.8047378541243643824, 0.8047378541243643824, 1.000000000000000000 ) ) 
 REPRESENTATION_ITEM ( '' )  );
#1833=CARTESIAN_POINT ( 'NONE',  ( 17.12895037488186389, -11.13829663063783215, 0.2687305842673423095 ) ) ;
#1838=EDGE_CURVE ( 'NONE', #3798, #13165, #8107, .T. ) ;
#1845=AXIS2_PLACEMENT_3D ( 'NONE', #6288, #2386, #4884 ) ;
#1847=EDGE_CURVE ( 'NONE', #4668, #14787, #1127, .T. ) ;
#1854=ORIENTED_EDGE ( 'NONE', *, *, #5396, .F. ) ;
#1875=EDGE_LOOP ( 'NONE', ( #14483, #1005, #11338, #4138 ) ) ;
#1878=ORIENTED_EDGE ( 'NONE', *, *, #2138, .T. ) ;
#1907=FACE_OUTER_BOUND ( 'NONE', #205, .T. ) ;
#1921=FACE_OUTER_BOUND ( 'NONE', #3534, .T. ) ;
#1922=( BOUNDED_CURVE ( )  B_SPLINE_CURVE ( 3, ( #2090, #6622, #1942, #6689 ),
 .UNSPECIFIED., .F., .T. ) 
 B_SPLINE_CURVE_WITH_KNOTS ( ( 4, 4 ),
 ( 1.570796326794896780, 3.141592653589795336 ),
 .UNSPECIFIED. ) 
 CURVE ( )  GEOMETRIC_REPRESENTATION_ITEM ( )  RATIONAL_B_SPLINE_CURVE ( ( 1.000000000000000000, 0.8047378541243644934, 0.8047378541243644934, 1.000000000000000000 ) ) 
 REPRESENTATION_ITEM ( '' )  );
#1923=FACE_OUTER_BOUND ( 'NONE', #2301, .T. ) ;
#1930=ORIENTED_EDGE ( 'NONE', *, *, #1823, .F. ) ;
#1931=EDGE_LOOP ( 'NONE', ( #1878, #2814, #12530, #10627 ) ) ;
#1933=EDGE_CURVE ( 'NONE', #14725, #14787, #2400, .T. ) ;
#1934=ORIENTED_EDGE ( 'NONE', *, *, #3377, .T. ) ;
#1942=CARTESIAN_POINT ( 'NONE',  ( 1.581646419014215876, 11.75147157172189871, 0.2664120436859918062 ) ) ;
#1946=CARTESIAN_POINT ( 'NONE',  ( 17.18164641901421419, 3.654316742536407592, 0.2664120436859910845 ) ) ;
#1950=ORIENTED_EDGE ( 'NONE', *, *, #6979, .T. ) ;
#1956=ADVANCED_FACE ( 'NONE', ( #2427 ), #1255, .F. ) ;
#1964=FACE_OUTER_BOUND ( 'NONE', #2098, .T. ) ;
#1978=CARTESIAN_POINT ( 'NONE',  ( 15.49557940054170047, -6.049654848385601793E-16, 18.93824625078692492 ) ) ;
#1996=EDGE_CURVE ( 'NONE', #15166, #14071, #3972, .T. ) ;
#2008=DIRECTION ( 'NONE',  ( 0.9999934663667179313, -5.016628125758410379E-17, 0.003614861529251473839 ) ) ;
#2014=CARTESIAN_POINT ( 'NONE',  ( 17.23697745638123280, 3.691760653673249681, -0.03314156585704653574 ) ) ;
#2021=ORIENTED_EDGE ( 'NONE', *, *, #10725, .T. ) ;
#2030=CARTESIAN_POINT ( 'NONE',  ( -12.81835358098578403, 11.99999970914576330, -11.73358795631400397 ) ) ;
#2038=AXIS2_PLACEMENT_3D ( 'NONE', #10878, #13437, #14287 ) ;
#2040=ORIENTED_EDGE ( 'NONE', *, *, #9155, .T. ) ;
#2041=DIRECTION ( 'NONE',  ( -0.000000000000000000, -4.336808689942017736E-16, 1.000000000000000000 ) ) ;
#2042=ADVANCED_FACE ( 'NONE', ( #13524 ), #5796, .T. ) ;
#2045=ORIENTED_EDGE ( 'NONE', *, *, #13227, .T. ) ;
#2055=DIRECTION ( 'NONE',  ( 0.000000000000000000, 1.387778780781444413E-14, -1.000000000000000000 ) ) ;
#2059=AXIS2_PLACEMENT_3D ( 'NONE', #4055, #8782, #9383 ) ;
#2075=VECTOR ( 'NONE', #2569, 999.9999999999998863 ) ;
#2090=CARTESIAN_POINT ( 'NONE',  ( 1.634139617129772404, 11.99999970914575798, -0.3335879563140091153 ) ) ;
#2098=EDGE_LOOP ( 'NONE', ( #5281, #776, #370, #7535 ) ) ;
#2108=CARTESIAN_POINT ( 'NONE',  ( 21.98164641901421135, -3.654316742536411589, 0.2664120436859909735 ) ) ;
#2111=DIRECTION ( 'NONE',  ( 0.1802821511763431361, 0.1220014872200674283, -0.9760194583528146728 ) ) ;
#2119=EDGE_LOOP ( 'NONE', ( #5408, #8599, #371, #12111 ) ) ;
#2125=EDGE_CURVE ( 'NONE', #6527, #6505, #1433, .T. ) ;
#2129=CARTESIAN_POINT ( 'NONE',  ( -9.503456061879928640, -12.00000029085427222, 69.60114695342350899 ) ) ;
#2135=CARTESIAN_POINT ( 'NONE',  ( 10.10045295220800554, -11.00000029085428110, 70.08978589960025829 ) ) ;
#2138=EDGE_CURVE ( 'NONE', #13430, #14951, #5047, .T. ) ;
#2144=CIRCLE ( 'NONE', #11822, 0.6000000000000000888 ) ;
#2159=ORIENTED_EDGE ( 'NONE', *, *, #14425, .T. ) ;
#2194=VERTEX_POINT ( 'NONE', #15044 ) ;
#2200=ORIENTED_EDGE ( 'NONE', *, *, #15107, .F. ) ;
#2221=CARTESIAN_POINT ( 'NONE',  ( -12.81835358098578403, -12.00000029085423670, -14.13358795631400611 ) ) ;
#2222=CARTESIAN_POINT ( 'NONE',  ( 17.04394838817069768, -11.40000029085424238, 0.2824263826447100945 ) ) ;
#2227=ORIENTED_EDGE ( 'NONE', *, *, #7968, .F. ) ;
#2229=ORIENTED_EDGE ( 'NONE', *, *, #6903, .T. ) ;
#2233=VERTEX_POINT ( 'NONE', #4505 ) ;
#2238=DIRECTION ( 'NONE',  ( -0.9961946980917452121, 0.000000000000000000, -0.08715574274766160756 ) ) ;
#2250=ORIENTED_EDGE ( 'NONE', *, *, #6853, .F. ) ;
#2256=DIRECTION ( 'NONE',  ( -0.000000000000000000, -1.000000000000000000, -0.000000000000000000 ) ) ;
#2261=PLANE ( 'NONE',  #6343 ) ;
#2272=EDGE_LOOP ( 'NONE', ( #3211, #14496, #5735, #11583 ) ) ;
#2274=DIRECTION ( 'NONE',  ( 4.710339085808869774E-17, 1.000000000000000000, -1.047133521511407648E-16 ) ) ;
#2276=DIRECTION ( 'NONE',  ( 1.000000000000000000, 0.000000000000000000, -0.000000000000000000 ) ) ;
#2297=PLANE ( 'NONE',  #9124 ) ;
#2301=EDGE_LOOP ( 'NONE', ( #7615, #9042, #6247, #1625 ) ) ;
#2307=ORIENTED_EDGE ( 'NONE', *, *, #5092, .F. ) ;
#2321=CARTESIAN_POINT ( 'NONE',  ( 21.98164641901421135, -11.40000029085423705, -8.183940086454239093 ) ) ;
#2323=VECTOR ( 'NONE', #14603, 1000.000000000000114 ) ;
#2327=ORIENTED_EDGE ( 'NONE', *, *, #12472, .F. ) ;
#2337=EDGE_CURVE ( 'NONE', #8985, #8702, #8988, .T. ) ;
#2342=CARTESIAN_POINT ( 'NONE',  ( 10.10406781373725771, 10.99999970914572778, 70.08979243323354069 ) ) ;
#2343=PLANE ( 'NONE',  #8757 ) ;
#2346=ORIENTED_EDGE ( 'NONE', *, *, #7434, .T. ) ;
#2358=CARTESIAN_POINT ( 'NONE',  ( -13.41835358098578723, 11.99999970914576330, -11.73358795631400753 ) ) ;
#2369=AXIS2_PLACEMENT_3D ( 'NONE', #13576, #1768, #601 ) ;
#2374=CARTESIAN_POINT ( 'NONE',  ( 21.98164641901421135, 12.59999970914575940, -8.183940086454237317 ) ) ;
#2375=VECTOR ( 'NONE', #2567, 1000.000000000000114 ) ;
#2381=ORIENTED_EDGE ( 'NONE', *, *, #137, .F. ) ;
#2386=DIRECTION ( 'NONE',  ( 1.000000000000000000, -0.000000000000000000, -0.000000000000000000 ) ) ;
#2398=DIRECTION ( 'NONE',  ( 0.08715574274766155205, 6.505213034913022660E-16, -0.9961946980917452121 ) ) ;
#2399=DIRECTION ( 'NONE',  ( 0.000000000000000000, -2.891205793294679017E-15, -1.000000000000000000 ) ) ;
#2400=CIRCLE ( 'NONE', #11083, 1.199999999999710854 ) ;
#2405=ORIENTED_EDGE ( 'NONE', *, *, #4909, .T. ) ;
#2406=CYLINDRICAL_SURFACE ( 'NONE', #7294, 1.000000000000000888 ) ;
#2412=DIRECTION ( 'NONE',  ( -0.08715574274766123286, 0.000000000000000000, 0.9961946980917453232 ) ) ;
#2425=( BOUNDED_CURVE ( )  B_SPLINE_CURVE ( 3, ( #9544, #10562, #11735, #5937 ),
 .UNSPECIFIED., .F., .T. ) 
 B_SPLINE_CURVE_WITH_KNOTS ( ( 4, 4 ),
 ( 3.141592653589792672, 4.712388980384706549 ),
 .UNSPECIFIED. ) 
 CURVE ( )  GEOMETRIC_REPRESENTATION_ITEM ( )  RATIONAL_B_SPLINE_CURVE ( ( 1.000000000000000000, 0.8047378541243609407, 0.8047378541243609407, 1.000000000000000000 ) ) 
 REPRESENTATION_ITEM ( '' )  );
#2427=FACE_OUTER_BOUND ( 'NONE', #5067, .T. ) ;
#2430=AXIS2_PLACEMENT_3D ( 'NONE', #13119, #1395, #2399 ) ;
#2444=ORIENTED_EDGE ( 'NONE', *, *, #4016, .F. ) ;
#2466=ADVANCED_FACE ( 'NONE', ( #13049 ), #2406, .T. ) ;
#2467=DIRECTION ( 'NONE',  ( 0.08715574274766160756, -6.299629708773494780E-18, -0.9961946980917452121 ) ) ;
#2475=ORIENTED_EDGE ( 'NONE', *, *, #5085, .T. ) ;
#2492=CARTESIAN_POINT ( 'NONE',  ( 17.18164641901421419, 11.99999970914575975, 0.8664120436859877872 ) ) ;
#2494=CARTESIAN_POINT ( 'NONE',  ( 16.12213235744115636, -12.00000029085424202, 0.3029999373072352897 ) ) ;
#2506=PLANE ( 'NONE',  #881 ) ;
#2508=CARTESIAN_POINT ( 'NONE',  ( 21.98164641901421135, -11.40000029085424238, 0.2664120436859911956 ) ) ;
#2528=( GEOMETRIC_REPRESENTATION_CONTEXT ( 3 ) GLOBAL_UNCERTAINTY_ASSIGNED_CONTEXT ( ( #936 ) ) GLOBAL_UNIT_ASSIGNED_CONTEXT ( ( #9896, #6439, #1754 ) ) REPRESENTATION_CONTEXT ( 'NONE', 'WORKASPACE' ) );
#2537=ORIENTED_EDGE ( 'NONE', *, *, #8355, .F. ) ;
#2562=ADVANCED_FACE ( 'NONE', ( #7614 ), #14574, .F. ) ;
#2565=CARTESIAN_POINT ( 'NONE',  ( 16.99691247867024657, -3.779330867977714892, 1.266532794505838000 ) ) ;
#2566=VECTOR ( 'NONE', #15021, 1000.000000000000000 ) ;
#2567=DIRECTION ( 'NONE',  ( 0.08715574274766155205, 6.505213034913022660E-16, -0.9961946980917452121 ) ) ;
#2569=DIRECTION ( 'NONE',  ( -0.08715574274766176022, -4.320305823558445788E-16, 0.9961946980917453232 ) ) ;
#2574=CARTESIAN_POINT ( 'NONE',  ( 16.21557691923156597, -12.00000029085576969, 0.2777084275547281322 ) ) ;
#2577=ORIENTED_EDGE ( 'NONE', *, *, #982, .F. ) ;
#2579=AXIS2_PLACEMENT_3D ( 'NONE', #11019, #391, #6458 ) ;
#2581=AXIS2_PLACEMENT_3D ( 'NONE', #9752, #7529, #375 ) ;
#2594=ADVANCED_FACE ( 'NONE', ( #383 ), #8836, .T. ) ;
#2603=CIRCLE ( 'NONE', #4348, 4.000000000000004441 ) ;
#2614=FACE_BOUND ( 'NONE', #11454, .T. ) ;
#2618=DIRECTION ( 'NONE',  ( 0.000000000000000000, -0.1666666666666656582, -0.9860132971832695770 ) ) ;
#2654=FACE_BOUND ( 'NONE', #7974, .T. ) ;
#2666=DIRECTION ( 'NONE',  ( -0.000000000000000000, 1.000000000000000000, 4.336808689942017736E-16 ) ) ;
#2678=VERTEX_POINT ( 'NONE', #8048 ) ;
#2686=DIRECTION ( 'NONE',  ( -0.000000000000000000, -4.336808689942017736E-16, 1.000000000000000000 ) ) ;
#2692=DIRECTION ( 'NONE',  ( 0.003614861529251474706, 0.000000000000000000, -0.9999934663667180423 ) ) ;
#2700=ORIENTED_EDGE ( 'NONE', *, *, #1821, .T. ) ;
#2706=EDGE_CURVE ( 'NONE', #9489, #4222, #6970, .T. ) ;
#2735=CARTESIAN_POINT ( 'NONE',  ( -13.41835358098578723, 11.99999970914576863, -56.77834603255778489 ) ) ;
#2752=EDGE_CURVE ( 'NONE', #8702, #12591, #329, .T. ) ;
#2760=CARTESIAN_POINT ( 'NONE',  ( -4.522482571421202024, 10.99999970914572778, 70.03692566716178192 ) ) ;
#2763=VECTOR ( 'NONE', #1798, 1000.000000000000000 ) ;
#2767=ORIENTED_EDGE ( 'NONE', *, *, #11386, .T. ) ;
#2772=EDGE_CURVE ( 'NONE', #4558, #134, #1824, .T. ) ;
#2780=FACE_OUTER_BOUND ( 'NONE', #10018, .T. ) ;
#2782=CIRCLE ( 'NONE', #6761, 1.000000000000000888 ) ;
#2789=ORIENTED_EDGE ( 'NONE', *, *, #12238, .F. ) ;
#2793=DIRECTION ( 'NONE',  ( -0.08715574274766164919, 0.000000000000000000, 0.9961946980917453232 ) ) ;
#2803=DIRECTION ( 'NONE',  ( 9.035018104045788110E-17, -0.9860132971832695770, 0.1666666666666656027 ) ) ;
#2814=ORIENTED_EDGE ( 'NONE', *, *, #10541, .T. ) ;
#2821=DIRECTION ( 'NONE',  ( 0.08715574274766167695, 0.000000000000000000, -0.9961946980917453232 ) ) ;
#2826=FACE_OUTER_BOUND ( 'NONE', #6846, .T. ) ;
#2828=FACE_OUTER_BOUND ( 'NONE', #4434, .T. ) ;
#2831=ORIENTED_EDGE ( 'NONE', *, *, #12760, .F. ) ;
#2840=CARTESIAN_POINT ( 'NONE',  ( -6.714472293954755422, -12.00000029085427578, 37.72291661448763733 ) ) ;
#2847=VERTEX_POINT ( 'NONE', #14249 ) ;
#2851=DIRECTION ( 'NONE',  ( -0.08715574274766162144, 0.000000000000000000, 0.9961946980917453232 ) ) ;
#2882=CARTESIAN_POINT ( 'NONE',  ( -9.503456061879925088, 11.99999970914574021, 69.60114695342350899 ) ) ;
#2890=ORIENTED_EDGE ( 'NONE', *, *, #3751, .T. ) ;
#2891=CIRCLE ( 'NONE', #5629, 4.000000000000004441 ) ;
#2909=DIRECTION ( 'NONE',  ( 0.000000000000000000, 0.000000000000000000, 1.000000000000000000 ) ) ;
#2917=DIRECTION ( 'NONE',  ( 0.000000000000000000, -1.000000000000000000, -4.336808689942017736E-16 ) ) ;
#2928=FACE_OUTER_BOUND ( 'NONE', #12607, .T. ) ;
#2945=DIRECTION ( 'NONE',  ( 0.000000000000000000, 0.000000000000000000, 1.000000000000000000 ) ) ;
#2949=ORIENTED_EDGE ( 'NONE', *, *, #3640, .F. ) ;
#2972=EDGE_CURVE ( 'NONE', #7121, #8647, #9908, .T. ) ;
#2973=ADVANCED_FACE ( 'NONE', ( #12166 ), #7379, .T. ) ;
#2982=ORIENTED_EDGE ( 'NONE', *, *, #8879, .T. ) ;
#2983=CARTESIAN_POINT ( 'NONE',  ( -12.81835358098578403, -12.60000029085423812, -8.183940086454239093 ) ) ;
#2988=VERTEX_POINT ( 'NONE', #6295 ) ;
#2991=DIRECTION ( 'NONE',  ( 1.000000000000000000, -0.000000000000000000, 0.000000000000000000 ) ) ;
#2996=LINE ( 'NONE', #14922, #959 ) ;
#3003=SHAPE_REPRESENTATION_RELATIONSHIP ( 'NONE' , 'NONE' ,  #11263, #10689 ) ;
#3008=ORIENTED_EDGE ( 'NONE', *, *, #1284, .F. ) ;
#3015=CYLINDRICAL_SURFACE ( 'NONE', #6271, 0.5999999999999998668 ) ;
#3016=EDGE_LOOP ( 'NONE', ( #1722, #13713, #11320, #6487 ) ) ;
#3041=ORIENTED_EDGE ( 'NONE', *, *, #8495, .T. ) ;
#3056=CARTESIAN_POINT ( 'NONE',  ( 22.58164641901421277, -2.908542350108650476E-07, -28.96834603255778262 ) ) ;
#3079=EDGE_CURVE ( 'NONE', #8700, #14725, #13189, .T. ) ;
#3088=( NAMED_UNIT ( * ) SI_UNIT ( $, .STERADIAN. ) SOLID_ANGLE_UNIT ( ) );
#3093=ORIENTED_EDGE ( 'NONE', *, *, #14175, .T. ) ;
#3096=EDGE_CURVE ( 'NONE', #11342, #14750, #4601, .T. ) ;
#3105=CIRCLE ( 'NONE', #869, 4.000000000000000888 ) ;
#3123=DIRECTION ( 'NONE',  ( 0.08715574274766123286, 0.000000000000000000, -0.9961946980917453232 ) ) ;
#3125=DIRECTION ( 'NONE',  ( 1.000000000000000000, 0.000000000000000000, 0.000000000000000000 ) ) ;
#3132=VECTOR ( 'NONE', #6499, 1000.000000000000000 ) ;
#3138=CARTESIAN_POINT ( 'NONE',  ( 17.12895037488186389, -3.654606557864051197, 0.2687305842673423095 ) ) ;
#3145=DIRECTION ( 'NONE',  ( 0.000000000000000000, -1.734723475976807686E-15, -1.000000000000000000 ) ) ;
#3146=ADVANCED_FACE ( 'NONE', ( #1921 ), #13574, .T. ) ;
#3155=CARTESIAN_POINT ( 'NONE',  ( 1.634139617129772404, 11.99999970914575798, -0.3335879563140091153 ) ) ;
#3177=CARTESIAN_POINT ( 'NONE',  ( -13.41835358098578723, -12.00000029085423137, -56.77834603255778489 ) ) ;
#3183=DIRECTION ( 'NONE',  ( -1.000000000000000000, 0.000000000000000000, 0.000000000000000000 ) ) ;
#3191=ORIENTED_EDGE ( 'NONE', *, *, #12541, .T. ) ;
#3197=ORIENTED_EDGE ( 'NONE', *, *, #7968, .T. ) ;
#3206=DIRECTION ( 'NONE',  ( 0.000000000000000000, 0.000000000000000000, -1.000000000000000000 ) ) ;
#3211=ORIENTED_EDGE ( 'NONE', *, *, #4281, .F. ) ;
#3214=CARTESIAN_POINT ( 'NONE',  ( 21.98164641901421135, -2.908542394189813650E-07, 0.2664120436859911956 ) ) ;
#3225=EDGE_CURVE ( 'NONE', #11747, #13723, #6074, .T. ) ;
#3228=CARTESIAN_POINT ( 'NONE',  ( 10.02391400960032009, -11.00000029085428110, 70.00595460678397330 ) ) ;
#3240=ORIENTED_EDGE ( 'NONE', *, *, #9252, .F. ) ;
#3242=ORIENTED_EDGE ( 'NONE', *, *, #576, .F. ) ;
#3243=VECTOR ( 'NONE', #340, 1000.000000000000000 ) ;
#3246=AXIS2_PLACEMENT_3D ( 'NONE', #8670, #5344, #6292 ) ;
#3247=CARTESIAN_POINT ( 'NONE',  ( -9.503456061879925088, 11.99999970914574021, 69.60114695342350899 ) ) ;
#3257=EDGE_CURVE ( 'NONE', #7951, #11859, #8526, .T. ) ;
#3270=DIRECTION ( 'NONE',  ( -1.000000000000000000, -0.000000000000000000, -0.000000000000000000 ) ) ;
#3290=DIRECTION ( 'NONE',  ( 0.000000000000000000, 1.047133521511407648E-16, 1.000000000000000000 ) ) ;
#3294=DIRECTION ( 'NONE',  ( -0.000000000000000000, -4.336808689942017736E-16, 1.000000000000000000 ) ) ;
#3295=LINE ( 'NONE', #10502, #9831 ) ;
#3296=VECTOR ( 'NONE', #6657, 1000.000000000000000 ) ;
#3299=ORIENTED_EDGE ( 'NONE', *, *, #610, .F. ) ;
#3309=TOROIDAL_SURFACE ( 'NONE', #5561, 2.400000000000000355, 0.6000000000000000888 ) ;
#3310=FACE_OUTER_BOUND ( 'NONE', #12128, .T. ) ;
#3315=DIRECTION ( 'NONE',  ( 0.000000000000000000, -0.1666666666666656582, 0.9860132971832695770 ) ) ;
#3317=AXIS2_PLACEMENT_3D ( 'NONE', #3228, #10060, #8977 ) ;
#3335=EDGE_CURVE ( 'NONE', #11131, #9085, #7313, .T. ) ;
#3358=VECTOR ( 'NONE', #13721, 1000.000000000000000 ) ;
#3366=ORIENTED_EDGE ( 'NONE', *, *, #2138, .F. ) ;
#3369=VECTOR ( 'NONE', #354, 1000.000000000000114 ) ;
#3377=EDGE_CURVE ( 'NONE', #134, #6145, #9032, .T. ) ;
#3396=AXIS2_PLACEMENT_3D ( 'NONE', #2983, #13549, #10106 ) ;
#3397=EDGE_LOOP ( 'NONE', ( #2159, #13691, #2537, #364 ) ) ;
#3423=CARTESIAN_POINT ( 'NONE',  ( 0.000000000000000000, 0.000000000000000000, 0.000000000000000000 ) ) ;
#3435=CARTESIAN_POINT ( 'NONE',  ( 21.98164641901421135, -11.40000029085423705, -11.73358795631401463 ) ) ;
#3437=VERTEX_POINT ( 'NONE', #9652 ) ;
#3440=ADVANCED_FACE ( 'NONE', ( #5104 ), #14473, .T. ) ;
#3446=CARTESIAN_POINT ( 'NONE',  ( -13.41835358098578723, -2.908542394189813650E-07, 0.2664120436859911956 ) ) ;
#3447=CYLINDRICAL_SURFACE ( 'NONE', #327, 0.6000000000000000888 ) ;
#3448=EDGE_CURVE ( 'NONE', #4566, #5234, #120, .T. ) ;
#3454=VERTEX_POINT ( 'NONE', #13249 ) ;
#3467=DIRECTION ( 'NONE',  ( 1.000000000000000000, -0.000000000000000000, 0.000000000000000000 ) ) ;
#3480=DIRECTION ( 'NONE',  ( 0.000000000000000000, -1.000000000000000000, 0.000000000000000000 ) ) ;
#3482=FACE_OUTER_BOUND ( 'NONE', #15277, .T. ) ;
#3492=AXIS2_PLACEMENT_3D ( 'NONE', #7653, #10974, #1352 ) ;
#3496=DIRECTION ( 'NONE',  ( 0.000000000000000000, 0.000000000000000000, 1.000000000000000000 ) ) ;
#3505=LINE ( 'NONE', #1104, #8498 ) ;
#3513=FACE_OUTER_BOUND ( 'NONE', #14123, .T. ) ;
#3520=DIRECTION ( 'NONE',  ( 0.9961946980917452121, -3.779777825264101491E-17, 0.08715574274766160756 ) ) ;
#3534=EDGE_LOOP ( 'NONE', ( #5590, #3008, #12588, #11899, #9005 ) ) ;
#3535=AXIS2_PLACEMENT_3D ( 'NONE', #444, #5182, #9891 ) ;
#3539=CARTESIAN_POINT ( 'NONE',  ( 21.98164641901421135, -12.00000029085423670, -11.73358795631400930 ) ) ;
#3541=DIRECTION ( 'NONE',  ( 0.000000000000000000, -0.9922779949676268085, -0.1240337885538713436 ) ) ;
#3544=EDGE_CURVE ( 'NONE', #13723, #3787, #268, .T. ) ;
#3550=FACE_OUTER_BOUND ( 'NONE', #4649, .T. ) ;
#3563=PLANE ( 'NONE',  #10828 ) ;
#3572=EDGE_CURVE ( 'NONE', #4992, #4558, #12012, .T. ) ;
#3587=CARTESIAN_POINT ( 'NONE',  ( -12.81835358098578403, 11.99999970914576686, -14.73358795631400575 ) ) ;
#3599=LINE ( 'NONE', #1339, #5253 ) ;
#3607=CARTESIAN_POINT ( 'NONE',  ( -13.41835358098578723, -11.40000029085424238, 0.2664120436859911956 ) ) ;
#3608=VECTOR ( 'NONE', #9506, 1000.000000000000000 ) ;
#3612=CARTESIAN_POINT ( 'NONE',  ( 16.75451632270442559, 11.78522852589359537, 0.2672856210392292042 ) ) ;
#3631=DIRECTION ( 'NONE',  ( 0.000000000000000000, 0.000000000000000000, -1.000000000000000000 ) ) ;
#3634=VERTEX_POINT ( 'NONE', #6784 ) ;
#3639=ORIENTED_EDGE ( 'NONE', *, *, #13072, .F. ) ;
#3640=EDGE_CURVE ( 'NONE', #6308, #7951, #13984, .T. ) ;
#3659=DIRECTION ( 'NONE',  ( -0.9999934663667180423, 1.567696289299852607E-18, -0.003614861529252313879 ) ) ;
#3666=CARTESIAN_POINT ( 'NONE',  ( 22.58164641901421632, -12.00000029085423137, -56.77834603255778489 ) ) ;
#3667=DIRECTION ( 'NONE',  ( 0.000000000000000000, 4.336808689942017736E-16, -1.000000000000000000 ) ) ;
#3669=DIRECTION ( 'NONE',  ( 0.000000000000000000, 0.1240337885538713436, -0.9922779949676268085 ) ) ;
#3670=DIRECTION ( 'NONE',  ( 0.000000000000000000, -1.000000000000000000, -4.336808689942017736E-16 ) ) ;
#3677=ADVANCED_FACE ( 'NONE', ( #1964 ), #5703, .F. ) ;
#3689=PRODUCT_CONTEXT ( 'NONE', #10906, 'mechanical' ) ;
#3691=AXIS2_PLACEMENT_3D ( 'NONE', #12765, #3294, #13629 ) ;
#3701=FACE_BOUND ( 'NONE', #836, .T. ) ;
#3706=VERTEX_POINT ( 'NONE', #7867 ) ;
#3725=ORIENTED_EDGE ( 'NONE', *, *, #8959, .F. ) ;
#3746=ORIENTED_EDGE ( 'NONE', *, *, #13059, .T. ) ;
#3750=TOROIDAL_SURFACE ( 'NONE', #5493, 2.400000000000000355, 0.6000000000000000888 ) ;
#3751=EDGE_CURVE ( 'NONE', #8660, #6308, #7094, .T. ) ;
#3758=DIRECTION ( 'NONE',  ( -1.000000000000000000, -0.000000000000000000, -0.000000000000000000 ) ) ;
#3762=CIRCLE ( 'NONE', #14153, 0.9999999999999991118 ) ;
#3787=VERTEX_POINT ( 'NONE', #8466 ) ;
#3798=VERTEX_POINT ( 'NONE', #1180 ) ;
#3800=AXIS2_PLACEMENT_3D ( 'NONE', #2358, #12912, #7111 ) ;
#3805=ORIENTED_EDGE ( 'NONE', *, *, #4215, .T. ) ;
#3819=CARTESIAN_POINT ( 'NONE',  ( 17.18107410701653137, 3.665822296182962958, 0.1743669014992922095 ) ) ;
#3824=ORIENTED_EDGE ( 'NONE', *, *, #13061, .T. ) ;
#3834=CARTESIAN_POINT ( 'NONE',  ( 22.58164641901421632, -12.00000029085423137, -56.77834603255778489 ) ) ;
#3844=EDGE_CURVE ( 'NONE', #13430, #6768, #13762, .T. ) ;
#3853=ADVANCED_FACE ( 'NONE', ( #12896 ), #2261, .T. ) ;
#3854=CARTESIAN_POINT ( 'NONE',  ( 22.28931995216796835, -12.00000029085427222, 69.13384072020834026 ) ) ;
#3858=LINE ( 'NONE', #8587, #8401 ) ;
#3861=DIRECTION ( 'NONE',  ( 0.000000000000000000, 0.000000000000000000, -1.000000000000000000 ) ) ;
#3864=CIRCLE ( 'NONE', #6363, 4.000000000000004441 ) ;
#3871=VERTEX_POINT ( 'NONE', #1644 ) ;
#3881=CARTESIAN_POINT ( 'NONE',  ( -13.41835358098578723, -12.00000029085423670, -11.73358795631400930 ) ) ;
#3900=ORIENTED_EDGE ( 'NONE', *, *, #5844, .T. ) ;
#3901=CARTESIAN_POINT ( 'NONE',  ( 16.59097840410232294, -11.89175346992432658, 0.2558260301694363359 ) ) ;
#3909=LINE ( 'NONE', #3834, #6850 ) ;
#3910=CARTESIAN_POINT ( 'NONE',  ( 21.98164641901421135, 11.99999970914576330, -14.13358795631400611 ) ) ;
#3911=CARTESIAN_POINT ( 'NONE',  ( 16.99691247867024657, 3.654316742536408924, 0.2664120436859911956 ) ) ;
#3914=CARTESIAN_POINT ( 'NONE',  ( 22.58164641901421632, -12.00000029085423670, -11.73358795631400930 ) ) ;
#3915=ORIENTED_EDGE ( 'NONE', *, *, #9240, .T. ) ;
#3917=EDGE_CURVE ( 'NONE', #8050, #7763, #2603, .T. ) ;
#3920=CARTESIAN_POINT ( 'NONE',  ( 22.58164641901421277, -3.779330867977713115, -28.96834603255778262 ) ) ;
#3924=AXIS2_PLACEMENT_3D ( 'NONE', #6916, #10148, #14879 ) ;
#3928=CARTESIAN_POINT ( 'NONE',  ( -1.733498803496027252, 11.99999970914575975, 38.15869532822594579 ) ) ;
#3929=CARTESIAN_POINT ( 'NONE',  ( -4.522482571421201136, -12.00000029085427222, 70.03692566716181034 ) ) ;
#3932=DIRECTION ( 'NONE',  ( -1.000000000000000000, 0.000000000000000000, -0.000000000000000000 ) ) ;
#3940=EDGE_CURVE ( 'NONE', #411, #856, #6208, .T. ) ;
#3941=LINE ( 'NONE', #11223, #13737 ) ;
#3972=LINE ( 'NONE', #6547, #15177 ) ;
#4003=FACE_BOUND ( 'NONE', #9476, .T. ) ;
#4005=CARTESIAN_POINT ( 'NONE',  ( 11.02372356922131758, -11.00000029085428110, 69.09311688316492450 ) ) ;
#4009=AXIS2_PLACEMENT_3D ( 'NONE', #7813, #7886, #1686 ) ;
#4016=EDGE_CURVE ( 'NONE', #11859, #12491, #4844, .T. ) ;
#4023=SURFACE_SIDE_STYLE ('',( #11310 ) ) ;
#4025=DIRECTION ( 'NONE',  ( 1.084202172485504434E-16, -1.000000000000000000, -0.000000000000000000 ) ) ;
#4032=ORIENTED_EDGE ( 'NONE', *, *, #137, .T. ) ;
#4055=CARTESIAN_POINT ( 'NONE',  ( 10.10406781373725948, -11.00000029085427933, 69.08979243323352648 ) ) ;
#4056=ORIENTED_EDGE ( 'NONE', *, *, #292, .T. ) ;
#4058=ORIENTED_EDGE ( 'NONE', *, *, #9979, .F. ) ;
#4062=VECTOR ( 'NONE', #2111, 1000.000000000000227 ) ;
#4073=AXIS2_PLACEMENT_3D ( 'NONE', #4727, #7214, #4891 ) ;
#4082=CARTESIAN_POINT ( 'NONE',  ( -13.16982544356192797, -12.00000029085424025, 0.01788390626213304940 ) ) ;
#4083=CARTESIAN_POINT ( 'NONE',  ( -3.127990687458618524, 2.260916199238038718E-16, 54.09781049769389227 ) ) ;
#4106=CARTESIAN_POINT ( 'NONE',  ( -1.733498803496028140, -12.00000029085427578, 38.15869532822594579 ) ) ;
#4108=ORIENTED_EDGE ( 'NONE', *, *, #980, .T. ) ;
#4123=DIRECTION ( 'NONE',  ( -0.000000000000000000, -0.000000000000000000, 1.000000000000000000 ) ) ;
#4138=ORIENTED_EDGE ( 'NONE', *, *, #3257, .T. ) ;
#4158=VERTEX_POINT ( 'NONE', #11484 ) ;
#4168=LINE ( 'NONE', #4314, #3132 ) ;
#4191=EDGE_LOOP ( 'NONE', ( #6328, #7079, #15276, #11995, #6286 ) ) ;
#4199=CARTESIAN_POINT ( 'NONE',  ( -13.41835358098578723, -12.00000029085423670, -11.73358795631401463 ) ) ;
#4215=EDGE_CURVE ( 'NONE', #4974, #3454, #14042, .T. ) ;
#4220=FACE_OUTER_BOUND ( 'NONE', #13671, .T. ) ;
#4222=VERTEX_POINT ( 'NONE', #14115 ) ;
#4224=ORIENTED_EDGE ( 'NONE', *, *, #1933, .F. ) ;
#4233=DIRECTION ( 'NONE',  ( 1.000000000000000000, 0.000000000000000000, 0.000000000000000000 ) ) ;
#4235=CARTESIAN_POINT ( 'NONE',  ( -13.41835358098578723, -12.00000029085423670, -14.13358795631400611 ) ) ;
#4243=CARTESIAN_POINT ( 'NONE',  ( 17.04394838817069768, -11.40000029085424238, 0.2824263826447100945 ) ) ;
#4251=CARTESIAN_POINT ( 'NONE',  ( -3.476613658449263955, 2.260916199238038718E-16, 58.08258929006087357 ) ) ;
#4281=EDGE_CURVE ( 'NONE', #3437, #9494, #9526, .T. ) ;
#4282=AXIS2_PLACEMENT_3D ( 'NONE', #13864, #8198, #15245 ) ;
#4285=CARTESIAN_POINT ( 'NONE',  ( 16.99691247867024657, -3.654316742536411589, 0.2664120436859911956 ) ) ;
#4298=EDGE_CURVE ( 'NONE', #14347, #7132, #13530, .T. ) ;
#4302=ORIENTED_EDGE ( 'NONE', *, *, #3940, .T. ) ;
#4303=ADVANCED_FACE ( 'NONE', ( #6071 ), #10784, .F. ) ;
#4314=CARTESIAN_POINT ( 'NONE',  ( -13.41835358098578723, 11.39999970914576366, -11.73358795631400397 ) ) ;
#4340=VERTEX_POINT ( 'NONE', #291 ) ;
#4348=AXIS2_PLACEMENT_3D ( 'NONE', #12124, #6242, #6397 ) ;
#4355=LINE ( 'NONE', #14817, #12222 ) ;
#4362=AXIS2_PLACEMENT_3D ( 'NONE', #6917, #1310, #4576 ) ;
#4369=AXIS2_PLACEMENT_3D ( 'NONE', #12188, #13515, #13438 ) ;
#4373=DIRECTION ( 'NONE',  ( 0.000000000000000000, 0.000000000000000000, -1.000000000000000000 ) ) ;
#4381=CIRCLE ( 'NONE', #12316, 0.9999999999999991118 ) ;
#4385=CARTESIAN_POINT ( 'NONE',  ( -3.127990687458618524, 2.260916199238038718E-16, 54.09781049769389227 ) ) ;
#4387=CARTESIAN_POINT ( 'NONE',  ( 22.58164641901421632, -11.40000029085423705, -11.73358795631401463 ) ) ;
#4401=CARTESIAN_POINT ( 'NONE',  ( 17.18164641901421419, -2.908542394189813650E-07, 0.2664120436859911956 ) ) ;
#4408=CARTESIAN_POINT ( 'NONE',  ( 17.12895037488186389, 10.99999970914575620, 0.2687305842673423095 ) ) ;
#4409=AXIS2_PLACEMENT_3D ( 'NONE', #2321, #9889, #4731 ) ;
#4410=ADVANCED_FACE ( 'NONE', ( #13271 ), #8807, .T. ) ;
#4416=ORIENTED_EDGE ( 'NONE', *, *, #10666, .F. ) ;
#4425=ADVANCED_FACE ( 'NONE', ( #2780 ), #10931, .T. ) ;
#4432=EDGE_LOOP ( 'NONE', ( #1361, #10020, #4224, #14251 ) ) ;
#4434=EDGE_LOOP ( 'NONE', ( #4861, #10356, #11362, #11266 ) ) ;
#4442=DIRECTION ( 'NONE',  ( -0.000000000000000000, 1.000000000000000000, 4.336808689942017736E-16 ) ) ;
#4450=DIRECTION ( 'NONE',  ( -0.000000000000000000, -1.000000000000000000, -0.000000000000000000 ) ) ;
#4468=ORIENTED_EDGE ( 'NONE', *, *, #3335, .T. ) ;
#4471=DIRECTION ( 'NONE',  ( -0.000000000000000000, -1.000000000000000000, -0.000000000000000000 ) ) ;
#4481=ORIENTED_EDGE ( 'NONE', *, *, #8959, .T. ) ;
#4483=ORIENTED_EDGE ( 'NONE', *, *, #6703, .F. ) ;
#4491=AXIS2_PLACEMENT_3D ( 'NONE', #8934, #2666, #8865 ) ;
#4502=EDGE_CURVE ( 'NONE', #11163, #3634, #9348, .T. ) ;
#4503=VERTEX_POINT ( 'NONE', #4251 ) ;
#4504=EDGE_CURVE ( 'NONE', #14951, #7919, #11381, .T. ) ;
#4505=CARTESIAN_POINT ( 'NONE',  ( 1.581646419014213878, 11.39999970914575655, 0.2664120436859911956 ) ) ;
#4507=EDGE_LOOP ( 'NONE', ( #14904, #10335, #3639, #11947 ) ) ;
#4527=STYLED_ITEM ( 'NONE', ( #4715 ), #10716 ) ;
#4537=CARTESIAN_POINT ( 'NONE',  ( 21.98164641901421135, -2.908542394189813650E-07, -0.3335879563140091153 ) ) ;
#4541=VECTOR ( 'NONE', #7026, 1000.000000000000000 ) ;
#4555=FACE_OUTER_BOUND ( 'NONE', #7057, .T. ) ;
#4556=EDGE_CURVE ( 'NONE', #7763, #8050, #3864, .T. ) ;
#4558=VERTEX_POINT ( 'NONE', #5585 ) ;
#4566=VERTEX_POINT ( 'NONE', #4106 ) ;
#4575=EDGE_CURVE ( 'NONE', #13856, #5737, #392, .T. ) ;
#4576=DIRECTION ( 'NONE',  ( 0.9961946980917453232, 0.000000000000000000, 0.08715574274766051122 ) ) ;
#4587=CARTESIAN_POINT ( 'NONE',  ( -12.81835358098578759, -12.00000029085424025, -8.183940086454239093 ) ) ;
#4601=( BOUNDED_CURVE ( )  B_SPLINE_CURVE ( 3, ( #12625, #13644, #5501, #14937 ),
 .UNSPECIFIED., .F., .T. ) 
 B_SPLINE_CURVE_WITH_KNOTS ( ( 4, 4 ),
 ( 1.753449257568233444, 2.075457819525424075 ),
 .UNSPECIFIED. ) 
 CURVE ( )  GEOMETRIC_REPRESENTATION_ITEM ( )  RATIONAL_B_SPLINE_CURVE ( ( 1.000000000000000000, 0.9913778568727538154, 0.9913778568727538154, 1.000000000000000000 ) ) 
 REPRESENTATION_ITEM ( '' )  );
#4606=ORIENTED_EDGE ( 'NONE', *, *, #1821, .F. ) ;
#4615=EDGE_CURVE ( 'NONE', #13053, #4566, #48, .T. ) ;
#4617=PLANE ( 'NONE',  #11936 ) ;
#4622=DIRECTION ( 'NONE',  ( 0.000000000000000000, -1.000000000000000000, 0.000000000000000000 ) ) ;
#4623=ORIENTED_EDGE ( 'NONE', *, *, #4016, .T. ) ;
#4626=CARTESIAN_POINT ( 'NONE',  ( 10.10406781373725948, 10.99999970914572778, 69.08979243323354069 ) ) ;
#4634=AXIS2_PLACEMENT_3D ( 'NONE', #12072, #14458, #12215 ) ;
#4649=EDGE_LOOP ( 'NONE', ( #11202, #14563, #13968, #10074 ) ) ;
#4665=CARTESIAN_POINT ( 'NONE',  ( -4.486254801108946033, -12.00000029085428110, 69.62284035768028900 ) ) ;
#4668=VERTEX_POINT ( 'NONE', #2222 ) ;
#4674=ADVANCED_FACE ( 'NONE', ( #4555 ), #4853, .T. ) ;
#4678=LINE ( 'NONE', #12739, #8483 ) ;
#4682=CARTESIAN_POINT ( 'NONE',  ( -7.760341206926691271, 5.861171052203402648E-16, 49.67725299158860253 ) ) ;
#4703=ADVANCED_FACE ( 'NONE', ( #7205 ), #9551, .T. ) ;
#4715=PRESENTATION_STYLE_ASSIGNMENT (( #9278 ) ) ;
#4717=CARTESIAN_POINT ( 'NONE',  ( -12.81835358098578403, 12.49999970914576153, -8.775548064764198131 ) ) ;
#4727=CARTESIAN_POINT ( 'NONE',  ( 22.58164641901421632, 12.59999970914575940, -8.183940086454237317 ) ) ;
#4729=LINE ( 'NONE', #11634, #11217 ) ;
#4731=DIRECTION ( 'NONE',  ( -1.000000000000000000, 0.000000000000000000, 0.000000000000000000 ) ) ;
#4737=CARTESIAN_POINT ( 'NONE',  ( 10.10406781373725771, -85.69524470659703752, 69.08979243323349806 ) ) ;
#4741=ORIENTED_EDGE ( 'NONE', *, *, #9718, .F. ) ;
#4767=AXIS2_PLACEMENT_3D ( 'NONE', #7786, #8075, #13969 ) ;
#4771=DIRECTION ( 'NONE',  ( 0.000000000000000000, 0.000000000000000000, -1.000000000000000000 ) ) ;
#4773=DIRECTION ( 'NONE',  ( -0.08715574274766176022, -4.320305823558445788E-16, 0.9961946980917453232 ) ) ;
#4775=CARTESIAN_POINT ( 'NONE',  ( 16.12213235758455809, 11.99999970914575798, 0.3029999356681916667 ) ) ;
#4776=VECTOR ( 'NONE', #2686, 1000.000000000000000 ) ;
#4778=EDGE_CURVE ( 'NONE', #6631, #8647, #10991, .T. ) ;
#4786=ADVANCED_FACE ( 'NONE', ( #4947 ), #7283, .T. ) ;
#4802=ORIENTED_EDGE ( 'NONE', *, *, #9354, .F. ) ;
#4806=ORIENTED_EDGE ( 'NONE', *, *, #876, .F. ) ;
#4816=VECTOR ( 'NONE', #4963, 1000.000000000000000 ) ;
#4825=CARTESIAN_POINT ( 'NONE',  ( -0.6310725616347281353, 2.041549731959705837E-17, 25.55790572381511794 ) ) ;
#4829=AXIS2_PLACEMENT_3D ( 'NONE', #8730, #15129, #9018 ) ;
#4844=CIRCLE ( 'NONE', #13270, 0.5999999999999999778 ) ;
#4845=DIRECTION ( 'NONE',  ( 0.000000000000000000, 1.000000000000000000, 0.000000000000000000 ) ) ;
#4849=CIRCLE ( 'NONE', #8311, 4.000000000000000888 ) ;
#4852=DIRECTION ( 'NONE',  ( 0.000000000000000000, 1.000000000000000000, 0.000000000000000000 ) ) ;
#4853=TOROIDAL_SURFACE ( 'NONE', #6837, 1.200000000000000178, 0.6000000000000000888 ) ;
#4861=ORIENTED_EDGE ( 'NONE', *, *, #6785, .F. ) ;
#4866=AXIS2_PLACEMENT_3D ( 'NONE', #12392, #1750, #584 ) ;
#4884=DIRECTION ( 'NONE',  ( 0.000000000000000000, 0.000000000000000000, 1.000000000000000000 ) ) ;
#4891=DIRECTION ( 'NONE',  ( 0.000000000000000000, 0.000000000000000000, -1.000000000000000000 ) ) ;
#4893=CARTESIAN_POINT ( 'NONE',  ( 22.58164641901421632, -12.00000029085424202, -0.3335879563140091153 ) ) ;
#4895=EDGE_CURVE ( 'NONE', #6527, #7325, #4168, .T. ) ;
#4897=DIRECTION ( 'NONE',  ( 0.000000000000000000, 1.734723475976805517E-15, -1.000000000000000000 ) ) ;
#4899=DIRECTION ( 'NONE',  ( -1.000000000000000000, -0.000000000000000000, -0.000000000000000000 ) ) ;
#4909=EDGE_CURVE ( 'NONE', #2233, #6527, #737, .T. ) ;
#4919=LINE ( 'NONE', #13141, #12778 ) ;
#4922=CARTESIAN_POINT ( 'NONE',  ( 16.75446144793115977, -11.78527509924292715, 0.2672796091214772463 ) ) ;
#4932=CARTESIAN_POINT ( 'NONE',  ( 17.18164641901421419, -12.00000029085424025, 0.8664120436859875651 ) ) ;
#4945=CARTESIAN_POINT ( 'NONE',  ( -13.41835358098578723, -12.40000029085423883, -9.367156043074160721 ) ) ;
#4947=FACE_OUTER_BOUND ( 'NONE', #13990, .T. ) ;
#4957=ORIENTED_EDGE ( 'NONE', *, *, #1047, .F. ) ;
#4958=ADVANCED_FACE ( 'NONE', ( #11295 ), #7670, .T. ) ;
#4960=LINE ( 'NONE', #12805, #1319 ) ;
#4963=DIRECTION ( 'NONE',  ( -1.000000000000000000, -0.000000000000000000, -0.000000000000000000 ) ) ;
#4974=VERTEX_POINT ( 'NONE', #1978 ) ;
#4979=FACE_OUTER_BOUND ( 'NONE', #10369, .T. ) ;
#4982=PLANE ( 'NONE',  #13970 ) ;
#4983=ADVANCED_FACE ( 'NONE', ( #12616 ), #6727, .T. ) ;
#4992=VERTEX_POINT ( 'NONE', #332 ) ;
#4999=DIRECTION ( 'NONE',  ( 0.9961946980917453232, -7.200509705930739692E-17, 0.08715574274766157981 ) ) ;
#5003=CYLINDRICAL_SURFACE ( 'NONE', #9011, 0.6000000000000000888 ) ;
#5019=DIRECTION ( 'NONE',  ( 0.000000000000000000, 0.000000000000000000, -1.000000000000000000 ) ) ;
#5029=CARTESIAN_POINT ( 'NONE',  ( 21.98164641901421135, 12.49999970914576153, -8.775548064764198131 ) ) ;
#5033=VERTEX_POINT ( 'NONE', #7570 ) ;
#5047=CIRCLE ( 'NONE', #2059, 1.000000000000000888 ) ;
#5058=EDGE_CURVE ( 'NONE', #7838, #3706, #3909, .T. ) ;
#5067=EDGE_LOOP ( 'NONE', ( #10922, #10890, #15099, #1930 ) ) ;
#5073=VECTOR ( 'NONE', #7450, 1000.000000000000000 ) ;
#5080=ADVANCED_FACE ( 'NONE', ( #12369 ), #494, .T. ) ;
#5083=CARTESIAN_POINT ( 'NONE',  ( -6.714472293954754534, 11.99999970914575975, 37.72291661448763733 ) ) ;
#5085=EDGE_CURVE ( 'NONE', #9494, #13360, #8817, .T. ) ;
#5092=EDGE_CURVE ( 'NONE', #6469, #3787, #2891, .T. ) ;
#5103=CARTESIAN_POINT ( 'NONE',  ( -6.714472293954755422, -12.00000029085427578, 37.72291661448763733 ) ) ;
#5104=FACE_OUTER_BOUND ( 'NONE', #13093, .T. ) ;
#5105=DIRECTION ( 'NONE',  ( -0.000000000000000000, -0.000000000000000000, -1.000000000000000000 ) ) ;
#5124=FACE_OUTER_BOUND ( 'NONE', #9103, .T. ) ;
#5127=DIRECTION ( 'NONE',  ( 1.000000000000000000, -0.000000000000000000, 0.000000000000000000 ) ) ;
#5136=ORIENTED_EDGE ( 'NONE', *, *, #9618, .F. ) ;
#5150=ORIENTED_EDGE ( 'NONE', *, *, #10541, .F. ) ;
#5152=ORIENTED_EDGE ( 'NONE', *, *, #8668, .T. ) ;
#5158=VECTOR ( 'NONE', #13544, 1000.000000000000000 ) ;
#5173=ORIENTED_EDGE ( 'NONE', *, *, #15106, .T. ) ;
#5176=DIRECTION ( 'NONE',  ( -1.000000000000000000, 0.000000000000000000, -0.000000000000000000 ) ) ;
#5178=LINE ( 'NONE', #5103, #12465 ) ;
#5182=DIRECTION ( 'NONE',  ( -0.9961946980917452121, 7.200509705930737227E-17, -0.08715574274766155205 ) ) ;
#5189=ORIENTED_EDGE ( 'NONE', *, *, #14175, .F. ) ;
#5226=DIRECTION ( 'NONE',  ( -1.000000000000000000, 0.000000000000000000, 0.000000000000000000 ) ) ;
#5234=VERTEX_POINT ( 'NONE', #11350 ) ;
#5253=VECTOR ( 'NONE', #8335, 1000.000000000000000 ) ;
#5262=EDGE_CURVE ( 'NONE', #12075, #6505, #13831, .T. ) ;
#5269=EDGE_CURVE ( 'NONE', #6473, #12431, #14896, .T. ) ;
#5281=ORIENTED_EDGE ( 'NONE', *, *, #4215, .F. ) ;
#5284=AXIS2_PLACEMENT_3D ( 'NONE', #11254, #4123, #3183 ) ;
#5286=DIRECTION ( 'NONE',  ( -0.9961946980917453232, 3.779777825264101491E-17, -0.08715574274766164919 ) ) ;
#5295=CARTESIAN_POINT ( 'NONE',  ( 11.95279236174586224, -8.891480818932939924E-16, 59.43248740176664313 ) ) ;
#5322=ORIENTED_EDGE ( 'NONE', *, *, #5269, .T. ) ;
#5344=DIRECTION ( 'NONE',  ( 0.000000000000000000, -0.000000000000000000, -1.000000000000000000 ) ) ;
#5347=CARTESIAN_POINT ( 'NONE',  ( -13.41835358098578723, 11.39999970914576188, -8.183940086454237317 ) ) ;
#5355=DIRECTION ( 'NONE',  ( 0.9961946980917452121, -3.779777825264104572E-17, 0.08715574274766174634 ) ) ;
#5365=ORIENTED_EDGE ( 'NONE', *, *, #1242, .T. ) ;
#5387=EDGE_LOOP ( 'NONE', ( #2045, #8049, #5907, #4623 ) ) ;
#5396=EDGE_CURVE ( 'NONE', #13723, #11747, #10304, .T. ) ;
#5408=ORIENTED_EDGE ( 'NONE', *, *, #11386, .F. ) ;
#5411=CARTESIAN_POINT ( 'NONE',  ( -9.503456061879928640, -12.00000029085427222, 69.60114695342350899 ) ) ;
#5419=DIRECTION ( 'NONE',  ( 0.000000000000000000, 1.000000000000000000, 0.000000000000000000 ) ) ;
#5430=PLANE ( 'NONE',  #948 ) ;
#5436=DIRECTION ( 'NONE',  ( 1.904272108403300901E-17, -1.000000000000000000, -6.513401669715868659E-16 ) ) ;
#5454=ORIENTED_EDGE ( 'NONE', *, *, #11256, .T. ) ;
#5479=ORIENTED_EDGE ( 'NONE', *, *, #8763, .F. ) ;
#5485=CARTESIAN_POINT ( 'NONE',  ( 22.58164641901421632, -11.40000029085423705, -8.183940086454239093 ) ) ;
#5488=CARTESIAN_POINT ( 'NONE',  ( -4.522482571421197584, 11.58578614677263197, 70.03692566716178192 ) ) ;
#5489=DIRECTION ( 'NONE',  ( -0.000000000000000000, -1.000000000000000000, -0.000000000000000000 ) ) ;
#5493=AXIS2_PLACEMENT_3D ( 'NONE', #5835, #7718, #11280 ) ;
#5501=CARTESIAN_POINT ( 'NONE',  ( 17.18107410701653137, -3.642811188889856666, 0.1743669014992923205 ) ) ;
#5531=CARTESIAN_POINT ( 'NONE',  ( -13.16982544356192797, 11.99999970914575975, 0.01788390626213397228 ) ) ;
#5538=PRODUCT_DEFINITION ( 'UNKNOWN', '', #12950, #7924 ) ;
#5561=AXIS2_PLACEMENT_3D ( 'NONE', #9410, #5882, #4771 ) ;
#5569=CARTESIAN_POINT ( 'NONE',  ( 17.18164641901421419, 11.39999970914575833, -0.3335879563140091153 ) ) ;
#5585=CARTESIAN_POINT ( 'NONE',  ( 22.58164641901421632, 12.39999970914576188, -9.367156043074160721 ) ) ;
#5586=CARTESIAN_POINT ( 'NONE',  ( -8.457587148907983021, 1.075975824879282337E-15, 57.64681057632257222 ) ) ;
#5590=ORIENTED_EDGE ( 'NONE', *, *, #3844, .T. ) ;
#5599=VECTOR ( 'NONE', #7979, 1000.000000000000114 ) ;
#5619=ADVANCED_FACE ( 'NONE', ( #14954 ), #8806, .T. ) ;
#5625=CARTESIAN_POINT ( 'NONE',  ( 17.18164641901421419, -3.654316742536411589, 0.2664120436859910845 ) ) ;
#5629=AXIS2_PLACEMENT_3D ( 'NONE', #14448, #4999, #2821 ) ;
#5630=DIRECTION ( 'NONE',  ( 1.000000000000000000, -0.000000000000000000, 0.000000000000000000 ) ) ;
#5632=LINE ( 'NONE', #14066, #10323 ) ;
#5633=EDGE_CURVE ( 'NONE', #8453, #5837, #12081, .T. ) ;
#5646=AXIS2_PLACEMENT_3D ( 'NONE', #7243, #11968, #14516 ) ;
#5667=APPLICATION_CONTEXT ( 'automotive_design' ) ;
#5678=ORIENTED_EDGE ( 'NONE', *, *, #10965, .F. ) ;
#5690=ORIENTED_EDGE ( 'NONE', *, *, #15106, .F. ) ;
#5692=ORIENTED_EDGE ( 'NONE', *, *, #8316, .F. ) ;
#5702=CARTESIAN_POINT ( 'NONE',  ( 22.58164641901421632, -12.00000029085423670, -11.73358795631401463 ) ) ;
#5703=CYLINDRICAL_SURFACE ( 'NONE', #4829, 4.000000000000000888 ) ;
#5718=CYLINDRICAL_SURFACE ( 'NONE', #11992, 0.6000000000000000888 ) ;
#5723=DIRECTION ( 'NONE',  ( 0.000000000000000000, 0.000000000000000000, 1.000000000000000000 ) ) ;
#5735=ORIENTED_EDGE ( 'NONE', *, *, #9039, .F. ) ;
#5737=VERTEX_POINT ( 'NONE', #6355 ) ;
#5743=ORIENTED_EDGE ( 'NONE', *, *, #15200, .T. ) ;
#5757=DIRECTION ( 'NONE',  ( 1.000000000000000000, -0.000000000000000000, -0.000000000000000000 ) ) ;
#5758=CARTESIAN_POINT ( 'NONE',  ( -4.522482571421201136, -12.00000029085427222, 70.03692566716181034 ) ) ;
#5772=FACE_OUTER_BOUND ( 'NONE', #8910, .T. ) ;
#5785=VERTEX_POINT ( 'NONE', #14694 ) ;
#5796=TOROIDAL_SURFACE ( 'NONE', #14447, 1.200000000000000178, 0.6000000000000000888 ) ;
#5804=EDGE_CURVE ( 'NONE', #4340, #9489, #336, .T. ) ;
#5811=CARTESIAN_POINT ( 'NONE',  ( 22.58164641901421632, 11.99999970914576330, -11.73358795631400397 ) ) ;
#5821=ORIENTED_EDGE ( 'NONE', *, *, #982, .T. ) ;
#5823=VERTEX_POINT ( 'NONE', #1602 ) ;
#5824=EDGE_CURVE ( 'NONE', #4974, #4158, #3105, .T. ) ;
#5830=AXIS2_PLACEMENT_3D ( 'NONE', #8005, #11503, #4373 ) ;
#5834=CARTESIAN_POINT ( 'NONE',  ( 17.14647606710965988, 3.654220075139516855, 0.2671853888517377595 ) ) ;
#5835=CARTESIAN_POINT ( 'NONE',  ( -12.81835358098578403, 11.99999970914576330, -11.73358795631400753 ) ) ;
#5836=LINE ( 'NONE', #5758, #6786 ) ;
#5837=VERTEX_POINT ( 'NONE', #1518 ) ;
#5844=EDGE_CURVE ( 'NONE', #6768, #14868, #1680, .T. ) ;
#5851=CARTESIAN_POINT ( 'NONE',  ( 22.58164641901421632, -3.579317323512964499, -0.3335879563140091153 ) ) ;
#5858=DIRECTION ( 'NONE',  ( -0.003614861529252313879, -4.336780354824422708E-16, 0.9999934663667180423 ) ) ;
#5862=VECTOR ( 'NONE', #7220, 1000.000000000000000 ) ;
#5863=LINE ( 'NONE', #9168, #7625 ) ;
#5864=EDGE_CURVE ( 'NONE', #4158, #15328, #14471, .T. ) ;
#5868=ORIENTED_EDGE ( 'NONE', *, *, #14059, .T. ) ;
#5878=LINE ( 'NONE', #8178, #9693 ) ;
#5879=LINE ( 'NONE', #10580, #6121 ) ;
#5882=DIRECTION ( 'NONE',  ( 1.000000000000000000, -0.000000000000000000, 0.000000000000000000 ) ) ;
#5897=DIRECTION ( 'NONE',  ( 0.000000000000000000, 0.000000000000000000, 1.000000000000000000 ) ) ;
#5899=DIRECTION ( 'NONE',  ( -1.000000000000000000, -0.000000000000000000, -0.000000000000000000 ) ) ;
#5900=FACE_BOUND ( 'NONE', #6018, .T. ) ;
#5907=ORIENTED_EDGE ( 'NONE', *, *, #9240, .F. ) ;
#5929=FACE_OUTER_BOUND ( 'NONE', #8639, .T. ) ;
#5937=CARTESIAN_POINT ( 'NONE',  ( 1.634139617129772404, -12.00000029085424025, -0.3335879563140197179 ) ) ;
#5941=DIRECTION ( 'NONE',  ( -0.000000000000000000, 4.336808689942017736E-16, -1.000000000000000000 ) ) ;
#5943=ORIENTED_EDGE ( 'NONE', *, *, #2772, .T. ) ;
#5961=VERTEX_POINT ( 'NONE', #5485 ) ;
#5967=ORIENTED_EDGE ( 'NONE', *, *, #12401, .F. ) ;
#5980=CYLINDRICAL_SURFACE ( 'NONE', #13497, 0.5999999999999998668 ) ;
#5982=ORIENTED_EDGE ( 'NONE', *, *, #3917, .F. ) ;
#5997=DIRECTION ( 'NONE',  ( -1.000000000000000000, 0.000000000000000000, -0.000000000000000000 ) ) ;
#6001=ORIENTED_EDGE ( 'NONE', *, *, #15071, .F. ) ;
#6017=DIRECTION ( 'NONE',  ( -0.08715574274766123286, 0.000000000000000000, 0.9961946980917453232 ) ) ;
#6018=EDGE_LOOP ( 'NONE', ( #4802, #2307 ) ) ;
#6019=ORIENTED_EDGE ( 'NONE', *, *, #1662, .T. ) ;
#6031=DIRECTION ( 'NONE',  ( 0.000000000000000000, 0.000000000000000000, 1.000000000000000000 ) ) ;
#6032=COLOUR_RGB ( '', 0.72549020, 0.75294118, 0.79215686) ;
#6033=ADVANCED_FACE ( 'NONE', ( #1196 ), #2506, .T. ) ;
#6037=CARTESIAN_POINT ( 'NONE',  ( 16.95294013567761837, 11.57155134438803223, 0.2884598355027922501 ) ) ;
#6048=DIRECTION ( 'NONE',  ( 1.000000000000000000, -0.000000000000000000, 0.000000000000000000 ) ) ;
#6054=ORIENTED_EDGE ( 'NONE', *, *, #14640, .F. ) ;
#6071=FACE_OUTER_BOUND ( 'NONE', #127, .T. ) ;
#6072=CLOSED_SHELL ( 'NONE', ( #15116, #6960, #2562, #15215, #9629, #10941, #10664, #18 ) ) ;
#6074=CIRCLE ( 'NONE', #8026, 4.000000000000004441 ) ;
#6077=ORIENTED_EDGE ( 'NONE', *, *, #4298, .F. ) ;
#6081=ORIENTED_EDGE ( 'NONE', *, *, #11101, .T. ) ;
#6082=DIRECTION ( 'NONE',  ( -0.9961946980917453232, 7.200509705930738460E-17, -0.08715574274766157981 ) ) ;
#6096=ORIENTED_EDGE ( 'NONE', *, *, #1838, .F. ) ;
#6114=LINE ( 'NONE', #9876, #7226 ) ;
#6119=VECTOR ( 'NONE', #3669, 1000.000000000000114 ) ;
#6121=VECTOR ( 'NONE', #3520, 1000.000000000000114 ) ;
#6124=ORIENTED_EDGE ( 'NONE', *, *, #3544, .T. ) ;
#6125=VECTOR ( 'NONE', #9037, 1000.000000000000000 ) ;
#6145=VERTEX_POINT ( 'NONE', #9563 ) ;
#6158=EDGE_CURVE ( 'NONE', #9613, #5234, #5879, .T. ) ;
#6159=CARTESIAN_POINT ( 'NONE',  ( 1.581646419014216542, -12.00000029085424202, 0.2664120436859911956 ) ) ;
#6167=FACE_OUTER_BOUND ( 'NONE', #1192, .T. ) ;
#6207=CARTESIAN_POINT ( 'NONE',  ( 21.98164641901421135, 11.39999970914575833, -0.3335879563140091153 ) ) ;
#6208=( BOUNDED_CURVE ( )  B_SPLINE_CURVE ( 3, ( #11030, #3819, #10884, #9929 ),
 .UNSPECIFIED., .F., .T. ) 
 B_SPLINE_CURVE_WITH_KNOTS ( ( 4, 4 ),
 ( 4.207727487654162601, 4.529736049611353010 ),
 .UNSPECIFIED. ) 
 CURVE ( )  GEOMETRIC_REPRESENTATION_ITEM ( )  RATIONAL_B_SPLINE_CURVE ( ( 1.000000000000000000, 0.9913778568727538154, 0.9913778568727538154, 1.000000000000000000 ) ) 
 REPRESENTATION_ITEM ( '' )  );
#6217=ORIENTED_EDGE ( 'NONE', *, *, #292, .F. ) ;
#6223=DIRECTION ( 'NONE',  ( 0.000000000000000000, 1.000000000000000000, 4.336808689942017736E-16 ) ) ;
#6226=ORIENTED_EDGE ( 'NONE', *, *, #5804, .F. ) ;
#6233=SPHERICAL_SURFACE ( 'NONE', #2579, 1.000000000000000000 ) ;
#6242=DIRECTION ( 'NONE',  ( 0.9961946980917452121, -3.779777825264104572E-17, 0.08715574274766174634 ) ) ;
#6245=TOROIDAL_SURFACE ( 'NONE', #8196, 1.200000000000000178, 0.6000000000000000888 ) ;
#6247=ORIENTED_EDGE ( 'NONE', *, *, #13341, .T. ) ;
#6249=VERTEX_POINT ( 'NONE', #12066 ) ;
#6253=EDGE_CURVE ( 'NONE', #11163, #12032, #1432, .T. ) ;
#6256=CIRCLE ( 'NONE', #14884, 0.5999999999999998668 ) ;
#6260=AXIS2_PLACEMENT_3D ( 'NONE', #13149, #10646, #9556 ) ;
#6271=AXIS2_PLACEMENT_3D ( 'NONE', #830, #12334, #1769 ) ;
#6274=CARTESIAN_POINT ( 'NONE',  ( 26.27204830164800953, -1.924145975121151140E-15, 27.91162381282022054 ) ) ;
#6280=DIRECTION ( 'NONE',  ( -0.000000000000000000, -1.000000000000000000, -0.000000000000000000 ) ) ;
#6286=ORIENTED_EDGE ( 'NONE', *, *, #11774, .T. ) ;
#6288=CARTESIAN_POINT ( 'NONE',  ( 17.18164641901421419, -11.40000029085424238, -0.3335879563140091153 ) ) ;
#6292=DIRECTION ( 'NONE',  ( 1.000000000000000000, 0.000000000000000000, 0.000000000000000000 ) ) ;
#6295=CARTESIAN_POINT ( 'NONE',  ( 17.18164641901421419, 11.99999970914575798, -0.3335879563140091153 ) ) ;
#6306=ORIENTED_EDGE ( 'NONE', *, *, #4575, .F. ) ;
#6308=VERTEX_POINT ( 'NONE', #1583 ) ;
#6318=FACE_OUTER_BOUND ( 'NONE', #7419, .T. ) ;
#6328=ORIENTED_EDGE ( 'NONE', *, *, #8174, .T. ) ;
#6332=CYLINDRICAL_SURFACE ( 'NONE', #10690, 4.000000000000004441 ) ;
#6338=LINE ( 'NONE', #11125, #5158 ) ;
#6343=AXIS2_PLACEMENT_3D ( 'NONE', #11736, #5858, #12984 ) ;
#6355=CARTESIAN_POINT ( 'NONE',  ( 17.04394838817069413, 11.39999970914576011, 0.2824263826447109826 ) ) ;
#6363=AXIS2_PLACEMENT_3D ( 'NONE', #8832, #5355, #829 ) ;
#6375=( NAMED_UNIT ( * ) PLANE_ANGLE_UNIT ( ) SI_UNIT ( $, .RADIAN. ) );
#6397=DIRECTION ( 'NONE',  ( 0.08715574274766167695, 0.000000000000000000, -0.9961946980917453232 ) ) ;
#6410=CARTESIAN_POINT ( 'NONE',  ( -13.41835358098578723, -11.40000029085424238, -0.3335879563140091153 ) ) ;
#6414=DIRECTION ( 'NONE',  ( 0.000000000000000000, 0.000000000000000000, 1.000000000000000000 ) ) ;
#6415=DIRECTION ( 'NONE',  ( 0.08715574274766167695, 0.000000000000000000, -0.9961946980917453232 ) ) ;
#6416=ORIENTED_EDGE ( 'NONE', *, *, #5058, .F. ) ;
#6439=( NAMED_UNIT ( * ) PLANE_ANGLE_UNIT ( ) SI_UNIT ( $, .RADIAN. ) );
#6458=DIRECTION ( 'NONE',  ( -1.000000000000000000, 1.734723475976808475E-15, 0.000000000000000000 ) ) ;
#6464=CARTESIAN_POINT ( 'NONE',  ( 22.58164641901421632, 12.49999970914576153, -8.775548064764198131 ) ) ;
#6469=VERTEX_POINT ( 'NONE', #10163 ) ;
#6473=VERTEX_POINT ( 'NONE', #5625 ) ;
#6487=ORIENTED_EDGE ( 'NONE', *, *, #6805, .F. ) ;
#6499=DIRECTION ( 'NONE',  ( 0.000000000000000000, 4.336808689942017736E-16, -1.000000000000000000 ) ) ;
#6505=VERTEX_POINT ( 'NONE', #1327 ) ;
#6519=CARTESIAN_POINT ( 'NONE',  ( 21.98164641901421135, 3.654316742536408924, 0.2664120436859909735 ) ) ;
#6520=EDGE_CURVE ( 'NONE', #11928, #14868, #7006, .T. ) ;
#6522=MECHANICAL_DESIGN_GEOMETRIC_PRESENTATION_REPRESENTATION('',(#8488),#13455);
#6527=VERTEX_POINT ( 'NONE', #167 ) ;
#6529=EDGE_LOOP ( 'NONE', ( #1704, #5821, #606, #7856 ) ) ;
#6547=CARTESIAN_POINT ( 'NONE',  ( 22.58164641901421632, -12.00000029085424025, -8.183940086454239093 ) ) ;
#6556=AXIS2_PLACEMENT_3D ( 'NONE', #466, #11162, #2945 ) ;
#6567=ORIENTED_EDGE ( 'NONE', *, *, #7434, .F. ) ;
#6572=CARTESIAN_POINT ( 'NONE',  ( -12.81835358098578403, 12.59999970914575940, -8.183940086454237317 ) ) ;
#6574=ADVANCED_FACE ( 'NONE', ( #5772 ), #9622, .F. ) ;
#6598=FILL_AREA_STYLE ('',( #12406 ) ) ;
#6601=CARTESIAN_POINT ( 'NONE',  ( 16.12213235758455809, 11.99999970914575798, 0.3029999356681916667 ) ) ;
#6603=CARTESIAN_POINT ( 'NONE',  ( -9.503456061879925088, 11.99999970914574021, 69.60114695342350899 ) ) ;
#6612=ORIENTED_EDGE ( 'NONE', *, *, #1662, .F. ) ;
#6622=CARTESIAN_POINT ( 'NONE',  ( 1.603389813606017178, 11.99999970914575798, 0.01788390626213483964 ) ) ;
#6628=CARTESIAN_POINT ( 'NONE',  ( 21.98164641901421135, -12.00000029085423670, -11.73358795631401463 ) ) ;
#6631=VERTEX_POINT ( 'NONE', #237 ) ;
#6657=DIRECTION ( 'NONE',  ( 0.000000000000000000, 4.336808689942017736E-16, -1.000000000000000000 ) ) ;
#6665=CARTESIAN_POINT ( 'NONE',  ( -0.2824495906440828152, 2.041549731959705837E-17, 21.57312693144813665 ) ) ;
#6673=CARTESIAN_POINT ( 'NONE',  ( 22.58164641901421632, 11.99999970914576330, -11.73358795631400397 ) ) ;
#6674=CARTESIAN_POINT ( 'NONE',  ( 22.58164641901421632, 3.729316161559856013, -0.3335879563140091153 ) ) ;
#6689=CARTESIAN_POINT ( 'NONE',  ( 1.581646419014213878, 11.39999970914575655, 0.2664120436859911956 ) ) ;
#6691=FACE_OUTER_BOUND ( 'NONE', #11264, .T. ) ;
#6703=EDGE_CURVE ( 'NONE', #8453, #5033, #1488, .T. ) ;
#6705=ADVANCED_FACE ( 'NONE', ( #14355 ), #7470, .T. ) ;
#6723=DIRECTION ( 'NONE',  ( -0.08715574274766167695, 0.000000000000000000, 0.9961946980917453232 ) ) ;
#6727=CYLINDRICAL_SURFACE ( 'NONE', #12549, 0.6000000000000000888 ) ;
#6743=CARTESIAN_POINT ( 'NONE',  ( 17.04394838817069413, 11.39999970914576011, 0.2824263826447109826 ) ) ;
#6745=CARTESIAN_POINT ( 'NONE',  ( -13.41835358098578723, -11.40000029085424238, 0.2664120436859911956 ) ) ;
#6761=AXIS2_PLACEMENT_3D ( 'NONE', #1396, #12249, #4897 ) ;
#6768=VERTEX_POINT ( 'NONE', #12421 ) ;
#6784=CARTESIAN_POINT ( 'NONE',  ( 22.58164641901421632, 3.729316161559856013, -0.3335879563140091153 ) ) ;
#6785=EDGE_CURVE ( 'NONE', #12175, #2233, #1922, .T. ) ;
#6786=VECTOR ( 'NONE', #7152, 1000.000000000000000 ) ;
#6790=ORIENTED_EDGE ( 'NONE', *, *, #13519, .F. ) ;
#6805=EDGE_CURVE ( 'NONE', #14347, #7919, #4381, .T. ) ;
#6813=EDGE_LOOP ( 'NONE', ( #1627, #6217 ) ) ;
#6826=CARTESIAN_POINT ( 'NONE',  ( -12.81835358098578759, -12.40000029085423883, -9.367156043074160721 ) ) ;
#6827=ORIENTED_EDGE ( 'NONE', *, *, #576, .T. ) ;
#6837=AXIS2_PLACEMENT_3D ( 'NONE', #11688, #3467, #3631 ) ;
#6846=EDGE_LOOP ( 'NONE', ( #5943, #1934, #2831, #3093 ) ) ;
#6848=ORIENTED_EDGE ( 'NONE', *, *, #14135, .T. ) ;
#6850=VECTOR ( 'NONE', #5226, 1000.000000000000000 ) ;
#6853=EDGE_CURVE ( 'NONE', #3706, #8985, #12580, .T. ) ;
#6886=FACE_OUTER_BOUND ( 'NONE', #2272, .T. ) ;
#6894=DIRECTION ( 'NONE',  ( 1.000000000000000000, -0.000000000000000000, 0.000000000000000000 ) ) ;
#6898=DIRECTION ( 'NONE',  ( 0.000000000000000000, 4.336808689942017736E-16, -1.000000000000000000 ) ) ;
#6903=EDGE_CURVE ( 'NONE', #9613, #8453, #1785, .T. ) ;
#6916=CARTESIAN_POINT ( 'NONE',  ( 21.98164641901421135, 11.39999970914576366, -11.73358795631400397 ) ) ;
#6917=CARTESIAN_POINT ( 'NONE',  ( 10.10406781373725771, 10.99999970914572600, 69.08979243323354069 ) ) ;
#6923=AXIS2_PLACEMENT_3D ( 'NONE', #8654, #5105, #14386 ) ;
#6936=FACE_OUTER_BOUND ( 'NONE', #3397, .T. ) ;
#6960=ADVANCED_FACE ( 'NONE', ( #3482 ), #3563, .F. ) ;
#6962=CARTESIAN_POINT ( 'NONE',  ( 11.02010870769206541, -11.00000029085428110, 70.09311034953164210 ) ) ;
#6963=DIRECTION ( 'NONE',  ( -0.000000000000000000, 1.000000000000000000, 4.336808689942017736E-16 ) ) ;
#6969=ORIENTED_EDGE ( 'NONE', *, *, #5262, .T. ) ;
#6970=LINE ( 'NONE', #6745, #2566 ) ;
#6977=CIRCLE ( 'NONE', #14632, 0.5999999999999998668 ) ;
#6979=EDGE_CURVE ( 'NONE', #5837, #13053, #8217, .T. ) ;
#6988=LINE ( 'NONE', #15268, #9558 ) ;
#6997=AXIS2_PLACEMENT_3D ( 'NONE', #14199, #3659, #8232 ) ;
#7000=AXIS2_PLACEMENT_3D ( 'NONE', #666, #5419, #14853 ) ;
#7004=CARTESIAN_POINT ( 'NONE',  ( 22.33311828159035883, -3.654316742536411144, 0.2664120436859908625 ) ) ;
#7006=LINE ( 'NONE', #10801, #13307 ) ;
#7026=DIRECTION ( 'NONE',  ( 1.000000000000000000, 0.000000000000000000, 0.000000000000000000 ) ) ;
#7027=CARTESIAN_POINT ( 'NONE',  ( -12.81835358098578403, 12.59999970914575940, -8.183940086454237317 ) ) ;
#7028=ORIENTED_EDGE ( 'NONE', *, *, #9680, .T. ) ;
#7055=AXIS2_PLACEMENT_3D ( 'NONE', #15242, #6894, #13935 ) ;
#7057=EDGE_LOOP ( 'NONE', ( #7080, #1239, #6612, #2982 ) ) ;
#7075=EDGE_CURVE ( 'NONE', #6527, #9489, #7296, .T. ) ;
#7079=ORIENTED_EDGE ( 'NONE', *, *, #876, .T. ) ;
#7080=ORIENTED_EDGE ( 'NONE', *, *, #13317, .T. ) ;
#7094=LINE ( 'NONE', #9323, #8037 ) ;
#7097=VECTOR ( 'NONE', #11208, 1000.000000000000114 ) ;
#7110=DIRECTION ( 'NONE',  ( 0.000000000000000000, -0.000000000000000000, 1.000000000000000000 ) ) ;
#7111=DIRECTION ( 'NONE',  ( 0.000000000000000000, 0.000000000000000000, -1.000000000000000000 ) ) ;
#7113=FACE_OUTER_BOUND ( 'NONE', #9865, .T. ) ;
#7117=CARTESIAN_POINT ( 'NONE',  ( 16.50219555133672955, 11.93237369474095999, 0.2532242768859266357 ) ) ;
#7121=VERTEX_POINT ( 'NONE', #14263 ) ;
#7127=DIRECTION ( 'NONE',  ( -1.000000000000000000, 0.000000000000000000, -0.000000000000000000 ) ) ;
#7128=CARTESIAN_POINT ( 'NONE',  ( -13.41835358098578723, 11.99999970914576863, -56.77834603255778489 ) ) ;
#7132=VERTEX_POINT ( 'NONE', #10615 ) ;
#7137=DIRECTION ( 'NONE',  ( 0.000000000000000000, 4.336808689942017736E-16, -1.000000000000000000 ) ) ;
#7145=DIRECTION ( 'NONE',  ( 7.228014483236693351E-17, 1.000000000000000000, 0.000000000000000000 ) ) ;
#7152=DIRECTION ( 'NONE',  ( 7.228014483236693351E-17, 1.000000000000000000, 0.000000000000000000 ) ) ;
#7154=DIRECTION ( 'NONE',  ( 0.000000000000000000, 1.000000000000000000, 4.336808689942017736E-16 ) ) ;
#7159=CYLINDRICAL_SURFACE ( 'NONE', #6997, 0.9999999999999957812 ) ;
#7184=ADVANCED_FACE ( 'NONE', ( #5124 ), #12246, .F. ) ;
#7189=CARTESIAN_POINT ( 'NONE',  ( -13.41835358098578723, 11.39999970914575833, -0.3335879563140091153 ) ) ;
#7194=EDGE_LOOP ( 'NONE', ( #9453, #14532, #9327, #6096 ) ) ;
#7199=LINE ( 'NONE', #10754, #9177 ) ;
#7205=FACE_OUTER_BOUND ( 'NONE', #9518, .T. ) ;
#7213=ORIENTED_EDGE ( 'NONE', *, *, #14564, .F. ) ;
#7214=DIRECTION ( 'NONE',  ( 1.000000000000000000, -0.000000000000000000, 0.000000000000000000 ) ) ;
#7220=DIRECTION ( 'NONE',  ( -0.000000000000000000, -1.000000000000000000, -0.000000000000000000 ) ) ;
#7226=VECTOR ( 'NONE', #10823, 1000.000000000000000 ) ;
#7243=CARTESIAN_POINT ( 'NONE',  ( 22.58164641901421632, -12.00000029085423670, -11.73358795631400930 ) ) ;
#7283=PLANE ( 'NONE',  #12296 ) ;
#7289=DIRECTION ( 'NONE',  ( 0.9961946980917452121, -7.200509705930739692E-17, 0.08715574274766157981 ) ) ;
#7294=AXIS2_PLACEMENT_3D ( 'NONE', #4737, #7154, #7832 ) ;
#7296=LINE ( 'NONE', #1155, #8350 ) ;
#7300=VECTOR ( 'NONE', #9210, 1000.000000000000000 ) ;
#7309=ORIENTED_EDGE ( 'NONE', *, *, #4281, .T. ) ;
#7313=CIRCLE ( 'NONE', #7806, 3.000000000000000888 ) ;
#7325=VERTEX_POINT ( 'NONE', #5347 ) ;
#7339=FACE_OUTER_BOUND ( 'NONE', #11803, .T. ) ;
#7346=EDGE_LOOP ( 'NONE', ( #9030, #3191, #10704, #7461 ) ) ;
#7360=DIRECTION ( 'NONE',  ( -0.9999934663667179313, 1.567696289299852222E-18, -0.003614861529252313445 ) ) ;
#7361=CARTESIAN_POINT ( 'NONE',  ( 11.02010870769206541, -11.00000029085428110, 70.09311034953164210 ) ) ;
#7371=ORIENTED_EDGE ( 'NONE', *, *, #14059, .F. ) ;
#7379=PLANE ( 'NONE',  #2581 ) ;
#7407=VECTOR ( 'NONE', #11174, 1000.000000000000000 ) ;
#7408=ORIENTED_EDGE ( 'NONE', *, *, #13152, .T. ) ;
#7412=DIRECTION ( 'NONE',  ( 1.000000000000000000, 0.000000000000000000, 0.000000000000000000 ) ) ;
#7417=EDGE_CURVE ( 'NONE', #3798, #5961, #14055, .T. ) ;
#7418=DIRECTION ( 'NONE',  ( 0.9961946980917453232, -7.200509705930739692E-17, 0.08715574274766157981 ) ) ;
#7419=EDGE_LOOP ( 'NONE', ( #9950, #11466, #8932, #1649, #7371, #8226, #10069, #12090 ) ) ;
#7432=DIRECTION ( 'NONE',  ( -0.08715574274766167695, 0.000000000000000000, 0.9961946980917453232 ) ) ;
#7434=EDGE_CURVE ( 'NONE', #6249, #2847, #14788, .T. ) ;
#7435=DIRECTION ( 'NONE',  ( -1.000000000000000000, -0.000000000000000000, -0.000000000000000000 ) ) ;
#7443=CYLINDRICAL_SURFACE ( 'NONE', #101, 4.000000000000004441 ) ;
#7450=DIRECTION ( 'NONE',  ( 0.000000000000000000, 1.000000000000000000, 4.336808689942017736E-16 ) ) ;
#7453=FACE_OUTER_BOUND ( 'NONE', #11319, .T. ) ;
#7456=ORIENTED_EDGE ( 'NONE', *, *, #4895, .F. ) ;
#7461=ORIENTED_EDGE ( 'NONE', *, *, #9200, .F. ) ;
#7470=PLANE ( 'NONE',  #4369 ) ;
#7486=FACE_OUTER_BOUND ( 'NONE', #10237, .T. ) ;
#7493=DIRECTION ( 'NONE',  ( 0.000000000000000000, -4.336808689942017736E-16, 1.000000000000000000 ) ) ;
#7496=CARTESIAN_POINT ( 'NONE',  ( -3.127990687458614971, 2.260916199238037239E-16, 54.09781049769389938 ) ) ;
#7513=FACE_OUTER_BOUND ( 'NONE', #12259, .T. ) ;
#7529=DIRECTION ( 'NONE',  ( 0.000000000000000000, -0.000000000000000000, 1.000000000000000000 ) ) ;
#7534=DIRECTION ( 'NONE',  ( -1.000000000000000000, -0.000000000000000000, -0.000000000000000000 ) ) ;
#7535=ORIENTED_EDGE ( 'NONE', *, *, #8184, .T. ) ;
#7537=AXIS2_PLACEMENT_3D ( 'NONE', #12762, #7882, #12614 ) ;
#7542=ORIENTED_EDGE ( 'NONE', *, *, #2125, .T. ) ;
#7544=EDGE_CURVE ( 'NONE', #1333, #6631, #6338, .T. ) ;
#7545=ORIENTED_EDGE ( 'NONE', *, *, #5396, .T. ) ;
#7550=PLANE ( 'NONE',  #2038 ) ;
#7559=DIRECTION ( 'NONE',  ( 0.000000000000000000, 0.000000000000000000, -1.000000000000000000 ) ) ;
#7570=CARTESIAN_POINT ( 'NONE',  ( -6.714472293954754534, 11.99999970914575975, 37.72291661448763733 ) ) ;
#7611=EDGE_CURVE ( 'NONE', #7838, #13165, #1731, .T. ) ;
#7612=FACE_OUTER_BOUND ( 'NONE', #9748, .T. ) ;
#7614=FACE_OUTER_BOUND ( 'NONE', #13076, .T. ) ;
#7615=ORIENTED_EDGE ( 'NONE', *, *, #5269, .F. ) ;
#7619=ORIENTED_EDGE ( 'NONE', *, *, #2337, .T. ) ;
#7625=VECTOR ( 'NONE', #15132, 1000.000000000000114 ) ;
#7639=EDGE_LOOP ( 'NONE', ( #1046, #11671, #12474, #10939 ) ) ;
#7652=CIRCLE ( 'NONE', #14569, 4.000000000000000888 ) ;
#7653=CARTESIAN_POINT ( 'NONE',  ( 21.98164641901421135, -11.40000029085424238, -0.3335879563140091153 ) ) ;
#7670=PLANE ( 'NONE',  #4866 ) ;
#7683=CARTESIAN_POINT ( 'NONE',  ( 22.58164641901420921, 3.685382519066023654, 0.01788390626213402432 ) ) ;
#7688=ORIENTED_EDGE ( 'NONE', *, *, #14820, .T. ) ;
#7690=EDGE_LOOP ( 'NONE', ( #11628, #1797, #6226, #3240 ) ) ;
#7693=DIRECTION ( 'NONE',  ( -0.08715574274766166307, -4.420346012544052123E-16, 0.9961946980917453232 ) ) ;
#7710=LINE ( 'NONE', #2735, #2763 ) ;
#7718=DIRECTION ( 'NONE',  ( 1.000000000000000000, -0.000000000000000000, 0.000000000000000000 ) ) ;
#7728=CIRCLE ( 'NONE', #6260, 4.000000000000000888 ) ;
#7729=DIRECTION ( 'NONE',  ( 0.000000000000000000, 0.000000000000000000, -1.000000000000000000 ) ) ;
#7733=CARTESIAN_POINT ( 'NONE',  ( -4.522482571421200248, 10.99999970914572422, 70.03692566716178192 ) ) ;
#7763=VERTEX_POINT ( 'NONE', #10248 ) ;
#7774=LINE ( 'NONE', #11258, #13339 ) ;
#7786=CARTESIAN_POINT ( 'NONE',  ( -6.714472293954755422, -12.00000029085427578, 37.72291661448763733 ) ) ;
#7787=AXIS2_PLACEMENT_3D ( 'NONE', #6826, #13941, #3315 ) ;
#7795=EDGE_LOOP ( 'NONE', ( #5173, #5152, #4957, #13891, #1568, #14773 ) ) ;
#7806=AXIS2_PLACEMENT_3D ( 'NONE', #3539, #9276, #11767 ) ;
#7808=SPHERICAL_SURFACE ( 'NONE', #822, 1.000000000000000000 ) ;
#7813=CARTESIAN_POINT ( 'NONE',  ( 17.21626540049105358, 10.99999970914576330, -12.20299797093197647 ) ) ;
#7818=ORIENTED_EDGE ( 'NONE', *, *, #7075, .F. ) ;
#7826=AXIS2_PLACEMENT_3D ( 'NONE', #147, #4899, #1078 ) ;
#7832=DIRECTION ( 'NONE',  ( 0.000000000000000000, 0.000000000000000000, 1.000000000000000000 ) ) ;
#7838=VERTEX_POINT ( 'NONE', #3666 ) ;
#7856=ORIENTED_EDGE ( 'NONE', *, *, #4778, .T. ) ;
#7867=CARTESIAN_POINT ( 'NONE',  ( -13.41835358098578723, -12.00000029085423137, -56.77834603255778489 ) ) ;
#7873=CARTESIAN_POINT ( 'NONE',  ( 16.12213235744115636, -12.00000029085424202, 0.3029999373072352897 ) ) ;
#7882=DIRECTION ( 'NONE',  ( -1.000000000000000000, 0.000000000000000000, -0.000000000000000000 ) ) ;
#7885=CARTESIAN_POINT ( 'NONE',  ( 21.98164641901421135, 11.39999970914575833, 0.2664120436859911956 ) ) ;
#7886=DIRECTION ( 'NONE',  ( -0.08715574274766174634, -4.320305823558445294E-16, 0.9961946980917452121 ) ) ;
#7899=ORIENTED_EDGE ( 'NONE', *, *, #9155, .F. ) ;
#7919=VERTEX_POINT ( 'NONE', #2342 ) ;
#7924=PRODUCT_DEFINITION_CONTEXT ( 'detailed design', #5667, 'design' ) ;
#7925=EDGE_CURVE ( 'NONE', #3798, #9085, #12829, .T. ) ;
#7938=ORIENTED_EDGE ( 'NONE', *, *, #12401, .T. ) ;
#7950=AXIS2_PLACEMENT_3D ( 'NONE', #8716, #9799, #12298 ) ;
#7951=VERTEX_POINT ( 'NONE', #3587 ) ;
#7962=DIRECTION ( 'NONE',  ( 0.000000000000000000, -0.000000000000000000, 1.000000000000000000 ) ) ;
#7963=CARTESIAN_POINT ( 'NONE',  ( 10.10406781373725771, -85.69524470659703752, 70.08979243323349806 ) ) ;
#7968=EDGE_CURVE ( 'NONE', #5785, #9613, #7774, .T. ) ;
#7970=AXIS2_PLACEMENT_3D ( 'NONE', #14057, #4442, #12661 ) ;
#7974=EDGE_LOOP ( 'NONE', ( #12632, #4741 ) ) ;
#7979=DIRECTION ( 'NONE',  ( 0.9961946980917452121, -3.779777825264101491E-17, 0.08715574274766160756 ) ) ;
#7993=ORIENTED_EDGE ( 'NONE', *, *, #5058, .T. ) ;
#8005=CARTESIAN_POINT ( 'NONE',  ( -12.81835358098578403, 11.99999970914576330, -14.13358795631400611 ) ) ;
#8019=ORIENTED_EDGE ( 'NONE', *, *, #7544, .F. ) ;
#8021=EDGE_CURVE ( 'NONE', #11859, #134, #13661, .T. ) ;
#8026=AXIS2_PLACEMENT_3D ( 'NONE', #15161, #1052, #10360 ) ;
#8037=VECTOR ( 'NONE', #13139, 1000.000000000000000 ) ;
#8043=DIRECTION ( 'NONE',  ( 0.000000000000000000, -1.000000000000000000, -4.336808689942017736E-16 ) ) ;
#8048=CARTESIAN_POINT ( 'NONE',  ( 17.12895037488186389, 10.99999970914575620, 0.2687305842673423095 ) ) ;
#8049=ORIENTED_EDGE ( 'NONE', *, *, #9332, .T. ) ;
#8050=VERTEX_POINT ( 'NONE', #5295 ) ;
#8075=DIRECTION ( 'NONE',  ( -0.08715574274766160756, 3.149814854386744309E-18, 0.9961946980917452121 ) ) ;
#8107=CIRCLE ( 'NONE', #5646, 2.400000000000001243 ) ;
#8108=AXIS2_PLACEMENT_3D ( 'NONE', #10432, #5897, #14096 ) ;
#8120=AXIS2_PLACEMENT_3D ( 'NONE', #8464, #169, #11961 ) ;
#8122=DIRECTION ( 'NONE',  ( 0.1802821511763431361, 0.1220014872200674283, -0.9760194583528146728 ) ) ;
#8128=DIRECTION ( 'NONE',  ( 0.000000000000000000, -4.336808689942017736E-16, 1.000000000000000000 ) ) ;
#8152=VERTEX_POINT ( 'NONE', #8996 ) ;
#8174=EDGE_CURVE ( 'NONE', #2678, #411, #927, .T. ) ;
#8178=CARTESIAN_POINT ( 'NONE',  ( 22.58164641901421632, -2.121185358860712356, -11.99873403588350307 ) ) ;
#8184=EDGE_CURVE ( 'NONE', #15328, #3454, #7652, .T. ) ;
#8196=AXIS2_PLACEMENT_3D ( 'NONE', #6572, #2991, #7729 ) ;
#8198=DIRECTION ( 'NONE',  ( -0.9961946980917452121, 7.200509705930737227E-17, -0.08715574274766155205 ) ) ;
#8217=LINE ( 'NONE', #1157, #11567 ) ;
#8220=CARTESIAN_POINT ( 'NONE',  ( 22.58164641901421632, -2.908542394189813650E-07, -0.3335879563140091153 ) ) ;
#8224=CARTESIAN_POINT ( 'NONE',  ( -4.522482571421200248, -11.00000029085428110, 70.03692566716176771 ) ) ;
#8226=ORIENTED_EDGE ( 'NONE', *, *, #6785, .T. ) ;
#8232=DIRECTION ( 'NONE',  ( -0.003614861529253208996, 0.000000000000000000, 0.9999934663667179313 ) ) ;
#8253=CARTESIAN_POINT ( 'NONE',  ( 10.10406781373725771, 10.99999970914572778, 69.08979243323354069 ) ) ;
#8257=ADVANCED_FACE ( 'NONE', ( #6691 ), #12800, .T. ) ;
#8261=CIRCLE ( 'NONE', #7537, 1.199999999999999734 ) ;
#8262=AXIS2_PLACEMENT_3D ( 'NONE', #6603, #5436, #10134 ) ;
#8266=( BOUNDED_CURVE ( )  B_SPLINE_CURVE ( 3, ( #11717, #4665, #1163, #8224 ),
 .UNSPECIFIED., .F., .T. ) 
 B_SPLINE_CURVE_WITH_KNOTS ( ( 4, 4 ),
 ( 1.570796326794897002, 3.141592653589793560 ),
 .UNSPECIFIED. ) 
 CURVE ( )  GEOMETRIC_REPRESENTATION_ITEM ( )  RATIONAL_B_SPLINE_CURVE ( ( 1.000000000000000000, 0.8047378541243649375, 0.8047378541243649375, 1.000000000000000000 ) ) 
 REPRESENTATION_ITEM ( '' )  );
#8289=VERTEX_POINT ( 'NONE', #12027 ) ;
#8310=ORIENTED_EDGE ( 'NONE', *, *, #3377, .F. ) ;
#8311=AXIS2_PLACEMENT_3D ( 'NONE', #6665, #13486, #2851 ) ;
#8316=EDGE_CURVE ( 'NONE', #14071, #9085, #9601, .T. ) ;
#8318=CARTESIAN_POINT ( 'NONE',  ( 21.98164641901421135, -3.654316742536411589, 0.2664120436859909735 ) ) ;
#8333=ORIENTED_EDGE ( 'NONE', *, *, #11101, .F. ) ;
#8335=DIRECTION ( 'NONE',  ( 1.000000000000000000, -0.000000000000000000, -0.000000000000000000 ) ) ;
#8349=CARTESIAN_POINT ( 'NONE',  ( 16.82707151287372227, 11.72089179802205727, 0.2761915063695380423 ) ) ;
#8350=VECTOR ( 'NONE', #3480, 1000.000000000000000 ) ;
#8354=ORIENTED_EDGE ( 'NONE', *, *, #1996, .F. ) ;
#8355=EDGE_CURVE ( 'NONE', #5961, #14071, #11102, .T. ) ;
#8370=ORIENTED_EDGE ( 'NONE', *, *, #151, .T. ) ;
#8401=VECTOR ( 'NONE', #7435, 1000.000000000000000 ) ;
#8403=CARTESIAN_POINT ( 'NONE',  ( 17.04394838817069768, -11.40000029085424238, 0.2824263826447100945 ) ) ;
#8412=DIRECTION ( 'NONE',  ( -1.740799290094577062E-15, -1.000000000000000000, -6.292789498690070142E-18 ) ) ;
#8416=ORIENTED_EDGE ( 'NONE', *, *, #10875, .T. ) ;
#8418=CARTESIAN_POINT ( 'NONE',  ( 17.04394838817069413, 11.39999970914576011, 0.2824263826447109826 ) ) ;
#8423=ORIENTED_EDGE ( 'NONE', *, *, #5633, .T. ) ;
#8427=LINE ( 'NONE', #6962, #13846 ) ;
#8429=FACE_OUTER_BOUND ( 'NONE', #7795, .T. ) ;
#8431=CARTESIAN_POINT ( 'NONE',  ( 21.98164641901421135, 12.39999970914576188, -9.367156043074160721 ) ) ;
#8448=LINE ( 'NONE', #6159, #1817 ) ;
#8453=VERTEX_POINT ( 'NONE', #1767 ) ;
#8464=CARTESIAN_POINT ( 'NONE',  ( 21.98164641901421135, -12.40000029085423883, -9.367156043074160721 ) ) ;
#8466=CARTESIAN_POINT ( 'NONE',  ( -2.779367716467965987, 2.260916199238035267E-16, 50.11303170532691098 ) ) ;
#8483=VECTOR ( 'NONE', #2256, 1000.000000000000000 ) ;
#8486=FACE_OUTER_BOUND ( 'NONE', #4191, .T. ) ;
#8488=STYLED_ITEM ( 'NONE', ( #13795 ), #10588 ) ;
#8489=DIRECTION ( 'NONE',  ( -1.000000000000000000, 0.000000000000000000, 0.000000000000000000 ) ) ;
#8495=EDGE_CURVE ( 'NONE', #12591, #12773, #12361, .T. ) ;
#8498=VECTOR ( 'NONE', #5941, 1000.000000000000000 ) ;
#8501=CARTESIAN_POINT ( 'NONE',  ( 21.98164641901421135, 11.99999970914576330, -11.73358795631400753 ) ) ;
#8507=DIRECTION ( 'NONE',  ( 0.000000000000000000, 0.000000000000000000, -1.000000000000000000 ) ) ;
#8521=CARTESIAN_POINT ( 'NONE',  ( 26.62067127263865274, -1.924145975121151140E-15, 23.92684502045323924 ) ) ;
#8526=CIRCLE ( 'NONE', #7055, 2.999999999999999112 ) ;
#8545=DIRECTION ( 'NONE',  ( 0.000000000000000000, -0.1666666666666656582, -0.9860132971832695770 ) ) ;
#8571=ORIENTED_EDGE ( 'NONE', *, *, #9332, .F. ) ;
#8578=ADVANCED_FACE ( 'NONE', ( #1923 ), #5430, .T. ) ;
#8587=CARTESIAN_POINT ( 'NONE',  ( 22.58164641901421632, -12.00000029085423314, -14.73358795631400575 ) ) ;
#8590=FACE_OUTER_BOUND ( 'NONE', #91, .T. ) ;
#8599=ORIENTED_EDGE ( 'NONE', *, *, #3448, .F. ) ;
#8633=DIRECTION ( 'NONE',  ( 0.000000000000000000, 0.000000000000000000, -1.000000000000000000 ) ) ;
#8635=AXIS2_PLACEMENT_3D ( 'NONE', #6673, #11380, #746 ) ;
#8637=ADVANCED_FACE ( 'NONE', ( #3310 ), #12561, .F. ) ;
#8638=CARTESIAN_POINT ( 'NONE',  ( 22.58164641901421632, -12.00000029085424202, -0.3335879563140091153 ) ) ;
#8639=EDGE_LOOP ( 'NONE', ( #13842, #15003, #753, #3824 ) ) ;
#8647=VERTEX_POINT ( 'NONE', #12626 ) ;
#8651=LINE ( 'NONE', #8810, #4776 ) ;
#8653=DIRECTION ( 'NONE',  ( 0.000000000000000000, -0.1240337885538713436, 0.9922779949676268085 ) ) ;
#8654=CARTESIAN_POINT ( 'NONE',  ( -12.81835358098578759, -11.40000029085423883, -8.183940086454239093 ) ) ;
#8660=VERTEX_POINT ( 'NONE', #7128 ) ;
#8668=EDGE_CURVE ( 'NONE', #13430, #8289, #8427, .T. ) ;
#8670=CARTESIAN_POINT ( 'NONE',  ( 21.98164641901421135, -11.40000029085424238, -0.3335879563140091153 ) ) ;
#8679=ADVANCED_FACE ( 'NONE', ( #14164 ), #2297, .T. ) ;
#8695=CARTESIAN_POINT ( 'NONE',  ( 17.18164641901421419, 11.39999970914575833, 0.2664120436859911956 ) ) ;
#8700=VERTEX_POINT ( 'NONE', #12935 ) ;
#8701=DIRECTION ( 'NONE',  ( 1.000000000000000000, -0.000000000000000000, -0.000000000000000000 ) ) ;
#8702=VERTEX_POINT ( 'NONE', #4945 ) ;
#8716=CARTESIAN_POINT ( 'NONE',  ( 21.98164641901421135, 12.59999970914575940, -8.183940086454237317 ) ) ;
#8723=ORIENTED_EDGE ( 'NONE', *, *, #4502, .T. ) ;
#8725=CARTESIAN_POINT ( 'NONE',  ( 22.58164641901421632, -11.40000029085424238, -0.3335879563140091153 ) ) ;
#8730=CARTESIAN_POINT ( 'NONE',  ( 26.62067127263865274, -1.924145975121151140E-15, 23.92684502045323924 ) ) ;
#8739=CIRCLE ( 'NONE', #1057, 0.6000000000000000888 ) ;
#8751=SURFACE_STYLE_USAGE ( .BOTH. , #4023 ) ;
#8753=DIRECTION ( 'NONE',  ( 0.000000000000000000, 0.000000000000000000, 1.000000000000000000 ) ) ;
#8757=AXIS2_PLACEMENT_3D ( 'NONE', #5702, #11886, #3667 ) ;
#8763=EDGE_CURVE ( 'NONE', #9085, #12591, #11686, .T. ) ;
#8764=ORIENTED_EDGE ( 'NONE', *, *, #3544, .F. ) ;
#8772=CIRCLE ( 'NONE', #4073, 1.199999999999999734 ) ;
#8773=CARTESIAN_POINT ( 'NONE',  ( -12.81835358098578403, -12.00000029085423314, -14.73358795631400575 ) ) ;
#8776=DIRECTION ( 'NONE',  ( -0.08715574274766157981, 1.084202172485503818E-16, 0.9961946980917452121 ) ) ;
#8781=ORIENTED_EDGE ( 'NONE', *, *, #4895, .T. ) ;
#8782=DIRECTION ( 'NONE',  ( 1.517216463963902273E-16, -1.000000000000000000, -1.734186353771755353E-15 ) ) ;
#8784=EDGE_LOOP ( 'NONE', ( #2475, #14393, #1687 ) ) ;
#8787=VECTOR ( 'NONE', #13340, 1000.000000000000000 ) ;
#8802=LINE ( 'NONE', #3920, #138 ) ;
#8806=TOROIDAL_SURFACE ( 'NONE', #10794, 2.400000000000000355, 0.6000000000000000888 ) ;
#8807=TOROIDAL_SURFACE ( 'NONE', #13284, 2.400000000000000355, 0.6000000000000000888 ) ;
#8809=CARTESIAN_POINT ( 'NONE',  ( -13.41835358098578723, -11.40000029085424416, 0.2664120436859911956 ) ) ;
#8810=CARTESIAN_POINT ( 'NONE',  ( -13.41835358098578723, -11.40000029085424238, 0.2664120436859911956 ) ) ;
#8817=CIRCLE ( 'NONE', #10289, 0.6000000000000000888 ) ;
#8832=CARTESIAN_POINT ( 'NONE',  ( 12.30141533273650900, -8.891480818932939924E-16, 55.44770860939965473 ) ) ;
#8836=CYLINDRICAL_SURFACE ( 'NONE', #6556, 1.000000000000000000 ) ;
#8839=EDGE_LOOP ( 'NONE', ( #536, #12837, #14390, #2405 ) ) ;
#8840=VECTOR ( 'NONE', #7145, 1000.000000000000000 ) ;
#8865=DIRECTION ( 'NONE',  ( 0.000000000000000000, 0.000000000000000000, -1.000000000000000000 ) ) ;
#8879=EDGE_CURVE ( 'NONE', #15166, #8152, #15320, .T. ) ;
#8882=DIRECTION ( 'NONE',  ( 1.001323786595528197E-17, -1.000000000000000000, -5.421010862427522786E-17 ) ) ;
#8887=CARTESIAN_POINT ( 'NONE',  ( -13.41835358098578723, -11.40000029085424416, 0.2664120436859911956 ) ) ;
#8910=EDGE_LOOP ( 'NONE', ( #12971, #7619, #10525, #3746, #7818, #8781, #9129, #1145, #14073, #20 ) ) ;
#8923=DIRECTION ( 'NONE',  ( -1.740799290094577062E-15, -1.000000000000000000, -6.292789498690070142E-18 ) ) ;
#8929=EDGE_LOOP ( 'NONE', ( #13869, #13805, #4481, #2021, #2250, #6416 ) ) ;
#8932=ORIENTED_EDGE ( 'NONE', *, *, #2972, .T. ) ;
#8934=CARTESIAN_POINT ( 'NONE',  ( 17.18164641901421419, -11.40000029085424238, 0.8664120436859875651 ) ) ;
#8938=DIRECTION ( 'NONE',  ( 0.000000000000000000, -1.000000000000000000, -4.336808689942017736E-16 ) ) ;
#8940=CIRCLE ( 'NONE', #11420, 0.5999999999999998668 ) ;
#8959=EDGE_CURVE ( 'NONE', #11131, #12773, #3858, .T. ) ;
#8973=ORIENTED_EDGE ( 'NONE', *, *, #1996, .T. ) ;
#8977=DIRECTION ( 'NONE',  ( -0.9961946980917453232, 0.000000000000000000, -0.08715574274766051122 ) ) ;
#8979=CARTESIAN_POINT ( 'NONE',  ( 22.33311828159035528, 3.654316742536409812, 0.2664120436859910290 ) ) ;
#8980=CARTESIAN_POINT ( 'NONE',  ( 17.10023064866893350, 11.27418174095661030, 0.2691555834469856467 ) ) ;
#8985=VERTEX_POINT ( 'NONE', #4235 ) ;
#8988=CIRCLE ( 'NONE', #10217, 2.400000000000001243 ) ;
#8996=CARTESIAN_POINT ( 'NONE',  ( -13.41835358098578723, -11.40000029085423705, -8.183940086454239093 ) ) ;
#9002=CARTESIAN_POINT ( 'NONE',  ( 17.23697745638123280, -3.616872831399570831, -0.03314156585704653574 ) ) ;
#9005=ORIENTED_EDGE ( 'NONE', *, *, #8668, .F. ) ;
#9009=ADVANCED_FACE ( 'NONE', ( #1907 ), #10189, .T. ) ;
#9011=AXIS2_PLACEMENT_3D ( 'NONE', #4932, #497, #6414 ) ;
#9018=DIRECTION ( 'NONE',  ( -0.08715574274766131613, 0.000000000000000000, 0.9961946980917453232 ) ) ;
#9028=EDGE_CURVE ( 'NONE', #8647, #3871, #1830, .T. ) ;
#9030=ORIENTED_EDGE ( 'NONE', *, *, #3940, .F. ) ;
#9032=CIRCLE ( 'NONE', #11763, 0.5999999999999998668 ) ;
#9035=CARTESIAN_POINT ( 'NONE',  ( -4.435020996998821019, 11.99999970914572778, 69.03723529703218276 ) ) ;
#9037=DIRECTION ( 'NONE',  ( -1.000000000000000000, 0.000000000000000000, 0.000000000000000000 ) ) ;
#9039=EDGE_CURVE ( 'NONE', #13360, #12431, #2996, .T. ) ;
#9042=ORIENTED_EDGE ( 'NONE', *, *, #14564, .T. ) ;
#9085=VERTEX_POINT ( 'NONE', #810 ) ;
#9103=EDGE_LOOP ( 'NONE', ( #1122, #3805, #4056, #10218 ) ) ;
#9124=AXIS2_PLACEMENT_3D ( 'NONE', #9653, #3541, #200 ) ;
#9126=( LENGTH_UNIT ( ) NAMED_UNIT ( * ) SI_UNIT ( .MILLI., .METRE. ) );
#9129=ORIENTED_EDGE ( 'NONE', *, *, #13227, .F. ) ;
#9155=EDGE_CURVE ( 'NONE', #9779, #7838, #1269, .T. ) ;
#9159=ADVANCED_FACE ( 'NONE', ( #7113 ), #5718, .T. ) ;
#9166=CARTESIAN_POINT ( 'NONE',  ( 22.58164641901421632, 11.99999970914576330, -11.73358795631400753 ) ) ;
#9168=CARTESIAN_POINT ( 'NONE',  ( 23.42650720483347371, -1.718469852516944459E-15, 60.43630737906597261 ) ) ;
#9169=ORIENTED_EDGE ( 'NONE', *, *, #5262, .F. ) ;
#9177=VECTOR ( 'NONE', #8122, 1000.000000000000227 ) ;
#9178=CARTESIAN_POINT ( 'NONE',  ( 22.58164641901421632, -12.00000029085423670, -14.13358795631400611 ) ) ;
#9189=ADVANCED_FACE ( 'NONE', ( #11907 ), #3309, .T. ) ;
#9200=EDGE_CURVE ( 'NONE', #856, #11342, #15307, .T. ) ;
#9210=DIRECTION ( 'NONE',  ( 0.000000000000000000, 1.000000000000000000, 0.000000000000000000 ) ) ;
#9232=DIRECTION ( 'NONE',  ( 0.9961946980917453232, -7.200509705930740925E-17, 0.08715574274766159368 ) ) ;
#9235=DIRECTION ( 'NONE',  ( -0.9961946980917453232, 7.200509705930739692E-17, -0.08715574274766156593 ) ) ;
#9237=CARTESIAN_POINT ( 'NONE',  ( -13.41835358098578723, 11.99999970914575975, -8.183940086454237317 ) ) ;
#9240=EDGE_CURVE ( 'NONE', #11859, #12075, #6977, .T. ) ;
#9246=ADVANCED_FACE ( 'NONE', ( #2826 ), #14385, .T. ) ;
#9252=EDGE_CURVE ( 'NONE', #11928, #4340, #12140, .T. ) ;
#9257=( BOUNDED_CURVE ( )  B_SPLINE_CURVE ( 3, ( #5851, #13134, #7004, #8318 ),
 .UNSPECIFIED., .F., .T. ) 
 B_SPLINE_CURVE_WITH_KNOTS ( ( 4, 4 ),
 ( 1.570796326794896780, 3.141592653589793116 ),
 .UNSPECIFIED. ) 
 CURVE ( )  GEOMETRIC_REPRESENTATION_ITEM ( )  RATIONAL_B_SPLINE_CURVE ( ( 1.000000000000000000, 0.8047378541243650485, 0.8047378541243650485, 1.000000000000000000 ) ) 
 REPRESENTATION_ITEM ( '' )  );
#9263=DIRECTION ( 'NONE',  ( 1.000000000000000000, 0.000000000000000000, 0.000000000000000000 ) ) ;
#9276=DIRECTION ( 'NONE',  ( -1.000000000000000000, 0.000000000000000000, -0.000000000000000000 ) ) ;
#9278=SURFACE_STYLE_USAGE ( .BOTH. , #978 ) ;
#9283=B_SPLINE_CURVE_WITH_KNOTS ( 'NONE', 3,
 ( #6743, #8980, #11464, #4408 ),
 .UNSPECIFIED., .F., .F.,
 ( 4, 4 ),
 ( 0.000000000000000000, 0.0004097632218424854624 ),
 .UNSPECIFIED. ) ;
#9312=VECTOR ( 'NONE', #7360, 1000.000000000000114 ) ;
#9317=ADVANCED_FACE ( 'NONE', ( #7339 ), #13313, .T. ) ;
#9323=CARTESIAN_POINT ( 'NONE',  ( -13.41835358098578723, 11.99999970914576330, -11.73358795631400397 ) ) ;
#9327=ORIENTED_EDGE ( 'NONE', *, *, #10190, .F. ) ;
#9332=EDGE_CURVE ( 'NONE', #7325, #12075, #8940, .T. ) ;
#9335=EDGE_CURVE ( 'NONE', #13360, #8700, #1764, .T. ) ;
#9338=EDGE_CURVE ( 'NONE', #1550, #6249, #6114, .T. ) ;
#9348=( BOUNDED_CURVE ( )  B_SPLINE_CURVE ( 3, ( #6519, #8979, #7683, #6674 ),
 .UNSPECIFIED., .F., .T. ) 
 B_SPLINE_CURVE_WITH_KNOTS ( ( 4, 4 ),
 ( 3.141592653589793116, 4.712388980384689674 ),
 .UNSPECIFIED. ) 
 CURVE ( )  GEOMETRIC_REPRESENTATION_ITEM ( )  RATIONAL_B_SPLINE_CURVE ( ( 1.000000000000000000, 0.8047378541243649375, 0.8047378541243649375, 1.000000000000000000 ) ) 
 REPRESENTATION_ITEM ( '' )  );
#9354=EDGE_CURVE ( 'NONE', #3787, #6469, #10926, .T. ) ;
#9358=FACE_OUTER_BOUND ( 'NONE', #2119, .T. ) ;
#9383=DIRECTION ( 'NONE',  ( 0.000000000000000000, 1.734723475976805517E-15, -1.000000000000000000 ) ) ;
#9384=ORIENTED_EDGE ( 'NONE', *, *, #22, .T. ) ;
#9400=ORIENTED_EDGE ( 'NONE', *, *, #10725, .F. ) ;
#9410=CARTESIAN_POINT ( 'NONE',  ( 21.98164641901421135, -12.00000029085423670, -11.73358795631400930 ) ) ;
#9419=ADVANCED_FACE ( 'NONE', ( #4220 ), #3750, .T. ) ;
#9424=AXIS2_PLACEMENT_3D ( 'NONE', #3914, #3758, #2909 ) ;
#9427=( NAMED_UNIT ( * ) PLANE_ANGLE_UNIT ( ) SI_UNIT ( $, .RADIAN. ) );
#9431=ORIENTED_EDGE ( 'NONE', *, *, #3225, .F. ) ;
#9432=DIRECTION ( 'NONE',  ( 0.000000000000000000, -0.9860132971832696880, 0.1666666666666656860 ) ) ;
#9436=DIRECTION ( 'NONE',  ( 0.08715574274766123286, 0.000000000000000000, -0.9961946980917453232 ) ) ;
#9443=VECTOR ( 'NONE', #9868, 1000.000000000000000 ) ;
#9446=DIRECTION ( 'NONE',  ( -0.9961946980917452121, 7.200509705930738460E-17, -0.08715574274766156593 ) ) ;
#9447=CARTESIAN_POINT ( 'NONE',  ( -9.503456061879928640, -12.00000029085427222, 69.60114695342350899 ) ) ;
#9449=CARTESIAN_POINT ( 'NONE',  ( 26.96929424362929950, -1.434287255462209759E-15, 19.94206622808625440 ) ) ;
#9453=ORIENTED_EDGE ( 'NONE', *, *, #7925, .T. ) ;
#9476=EDGE_LOOP ( 'NONE', ( #1854, #9431 ) ) ;
#9480=AXIS2_PLACEMENT_3D ( 'NONE', #14306, #11984, #100 ) ;
#9486=CARTESIAN_POINT ( 'NONE',  ( 11.10026251182900481, -11.00000029085427933, 69.17694817598119528 ) ) ;
#9488=CARTESIAN_POINT ( 'NONE',  ( 22.58164641901421632, 11.99999970914576863, -56.77834603255778489 ) ) ;
#9489=VERTEX_POINT ( 'NONE', #8887 ) ;
#9494=VERTEX_POINT ( 'NONE', #8725 ) ;
#9495=VECTOR ( 'NONE', #4622, 1000.000000000000000 ) ;
#9506=DIRECTION ( 'NONE',  ( -3.614007241618342978E-17, -1.000000000000000000, -0.000000000000000000 ) ) ;
#9511=VECTOR ( 'NONE', #1417, 999.9999999999998863 ) ;
#9514=LINE ( 'NONE', #13260, #8787 ) ;
#9517=ORIENTED_EDGE ( 'NONE', *, *, #12760, .T. ) ;
#9518=EDGE_LOOP ( 'NONE', ( #13029, #8333, #7938, #6306 ) ) ;
#9526=LINE ( 'NONE', #8220, #5862 ) ;
#9533=ORIENTED_EDGE ( 'NONE', *, *, #10875, .F. ) ;
#9541=FACE_OUTER_BOUND ( 'NONE', #12728, .T. ) ;
#9542=DIRECTION ( 'NONE',  ( -0.08715574274766164919, -4.320305823558445788E-16, 0.9961946980917453232 ) ) ;
#9544=CARTESIAN_POINT ( 'NONE',  ( 1.581646419014216542, -11.40000029085424238, 0.2664120436859911956 ) ) ;
#9551=TOROIDAL_SURFACE ( 'NONE', #11066, 1.200000000000000178, 0.6000000000000000888 ) ;
#9556=DIRECTION ( 'NONE',  ( 0.08715574274766176022, 0.000000000000000000, -0.9961946980917453232 ) ) ;
#9558=VECTOR ( 'NONE', #5757, 1000.000000000000000 ) ;
#9563=CARTESIAN_POINT ( 'NONE',  ( 21.98164641901421135, 11.99999970914575975, -8.183940086454237317 ) ) ;
#9570=CARTESIAN_POINT ( 'NONE',  ( 16.31442355444756132, 11.98691892176511331, 0.2637538782190264053 ) ) ;
#9571=VECTOR ( 'NONE', #11561, 1000.000000000000000 ) ;
#9601=CIRCLE ( 'NONE', #2430, 0.5999999999999998668 ) ;
#9607=ADVANCED_FACE ( 'NONE', ( #14775 ), #6245, .T. ) ;
#9613=VERTEX_POINT ( 'NONE', #5411 ) ;
#9618=EDGE_CURVE ( 'NONE', #134, #455, #1273, .T. ) ;
#9622=PLANE ( 'NONE',  #1136 ) ;
#9624=LINE ( 'NONE', #13290, #9511 ) ;
#9629=ADVANCED_FACE ( 'NONE', ( #15224 ), #4617, .F. ) ;
#9634=CYLINDRICAL_SURFACE ( 'NONE', #14651, 0.6000000000000000888 ) ;
#9652=CARTESIAN_POINT ( 'NONE',  ( 22.58164641901421632, -3.579317323512964499, -0.3335879563140091153 ) ) ;
#9653=CARTESIAN_POINT ( 'NONE',  ( 16.99691247867024657, 3.529302617095105621, 1.266532794505838000 ) ) ;
#9669=DIRECTION ( 'NONE',  ( -0.08715574274766131613, 0.000000000000000000, 0.9961946980917453232 ) ) ;
#9673=CYLINDRICAL_SURFACE ( 'NONE', #12959, 1.000000000000000888 ) ;
#9680=EDGE_CURVE ( 'NONE', #1533, #3437, #5878, .T. ) ;
#9684=ORIENTED_EDGE ( 'NONE', *, *, #448, .F. ) ;
#9693=VECTOR ( 'NONE', #10579, 1000.000000000000114 ) ;
#9695=CARTESIAN_POINT ( 'NONE',  ( 1.634139617129772404, -85.69524470659700910, -0.3335879563140516924 ) ) ;
#9701=DIRECTION ( 'NONE',  ( 0.000000000000000000, 0.000000000000000000, -1.000000000000000000 ) ) ;
#9712=EDGE_CURVE ( 'NONE', #11163, #1167, #10344, .T. ) ;
#9713=DIRECTION ( 'NONE',  ( 0.000000000000000000, -1.000000000000000000, 0.000000000000000000 ) ) ;
#9718=EDGE_CURVE ( 'NONE', #2194, #4503, #10937, .T. ) ;
#9748=EDGE_LOOP ( 'NONE', ( #3915, #2327, #8310, #9918 ) ) ;
#9752=CARTESIAN_POINT ( 'NONE',  ( -13.41835358098578723, -2.908542394189813650E-07, 0.2664120436859911956 ) ) ;
#9753=DIRECTION ( 'NONE',  ( 1.000000000000000000, -0.000000000000000000, 0.000000000000000000 ) ) ;
#9779=VERTEX_POINT ( 'NONE', #11518 ) ;
#9784=ORIENTED_EDGE ( 'NONE', *, *, #4504, .T. ) ;
#9788=LINE ( 'NONE', #14521, #9443 ) ;
#9791=DIRECTION ( 'NONE',  ( 0.000000000000000000, 0.000000000000000000, -1.000000000000000000 ) ) ;
#9799=DIRECTION ( 'NONE',  ( 1.000000000000000000, -0.000000000000000000, 0.000000000000000000 ) ) ;
#9808=ORIENTED_EDGE ( 'NONE', *, *, #9886, .T. ) ;
#9818=CARTESIAN_POINT ( 'NONE',  ( 16.99691247867024657, -3.779330867977714892, 1.266532794505838000 ) ) ;
#9831=VECTOR ( 'NONE', #4773, 999.9999999999998863 ) ;
#9848=( BOUNDED_CURVE ( )  B_SPLINE_CURVE ( 3, ( #15150, #11602, #1042, #10351 ),
 .UNSPECIFIED., .F., .T. ) 
 B_SPLINE_CURVE_WITH_KNOTS ( ( 4, 4 ),
 ( 0.000000000000000000, 0.08794004307218132588 ),
 .UNSPECIFIED. ) 
 CURVE ( )  GEOMETRIC_REPRESENTATION_ITEM ( )  RATIONAL_B_SPLINE_CURVE ( ( 1.000000000000000000, 0.9993556495590054656, 0.9993556495590054656, 1.000000000000000000 ) ) 
 REPRESENTATION_ITEM ( '' )  );
#9859=CARTESIAN_POINT ( 'NONE',  ( 21.98164641901421135, 3.654316742536408924, 0.2664120436859909735 ) ) ;
#9865=EDGE_LOOP ( 'NONE', ( #5365, #3242, #1548, #10332 ) ) ;
#9868=DIRECTION ( 'NONE',  ( -2.345198365613508922E-35, -1.000000000000000000, -4.336808689942017736E-16 ) ) ;
#9876=CARTESIAN_POINT ( 'NONE',  ( 22.58164641901421632, 11.39999970914575833, 0.2664120436859911956 ) ) ;
#9886=EDGE_CURVE ( 'NONE', #7919, #6631, #3762, .T. ) ;
#9887=DIRECTION ( 'NONE',  ( 0.9961946980917452121, -3.779777825264101491E-17, 0.08715574274766160756 ) ) ;
#9889=DIRECTION ( 'NONE',  ( 0.000000000000000000, 0.000000000000000000, -1.000000000000000000 ) ) ;
#9891=DIRECTION ( 'NONE',  ( -0.08715574274766155205, 0.000000000000000000, 0.9961946980917452121 ) ) ;
#9895=ORIENTED_EDGE ( 'NONE', *, *, #3448, .T. ) ;
#9896=( LENGTH_UNIT ( ) NAMED_UNIT ( * ) SI_UNIT ( .MILLI., .METRE. ) );
#9904=CARTESIAN_POINT ( 'NONE',  ( 11.10026251182900303, 10.99999970914572600, 69.17694817598120949 ) ) ;
#9908=LINE ( 'NONE', #13266, #5073 ) ;
#9918=ORIENTED_EDGE ( 'NONE', *, *, #8021, .F. ) ;
#9928=CARTESIAN_POINT ( 'NONE',  ( 11.02010870769206541, 10.99999970914572600, 70.09311034953165631 ) ) ;
#9929=CARTESIAN_POINT ( 'NONE',  ( 17.23697745638123280, 3.691760653673249681, -0.03314156585704653574 ) ) ;
#9933=CARTESIAN_POINT ( 'NONE',  ( -13.41835358098578723, 11.39999970914575833, 0.2664120436859911956 ) ) ;
#9942=CARTESIAN_POINT ( 'NONE',  ( -13.41835358098578723, -11.40000029085424238, -0.3335879563140091153 ) ) ;
#9950=ORIENTED_EDGE ( 'NONE', *, *, #6520, .T. ) ;
#9979=EDGE_CURVE ( 'NONE', #455, #4992, #6256, .T. ) ;
#10018=EDGE_LOOP ( 'NONE', ( #2346, #4108, #9533 ) ) ;
#10020=ORIENTED_EDGE ( 'NONE', *, *, #1847, .T. ) ;
#10043=DIRECTION ( 'NONE',  ( 0.000000000000000000, 1.000000000000000000, 0.000000000000000000 ) ) ;
#10047=DIRECTION ( 'NONE',  ( 1.000000000000000000, -0.000000000000000000, -0.000000000000000000 ) ) ;
#10057=AXIS2_PLACEMENT_3D ( 'NONE', #6207, #14476, #3861 ) ;
#10060=DIRECTION ( 'NONE',  ( 0.08715574274766174634, 4.320305823558445294E-16, -0.9961946980917452121 ) ) ;
#10069=ORIENTED_EDGE ( 'NONE', *, *, #11612, .T. ) ;
#10074=ORIENTED_EDGE ( 'NONE', *, *, #11402, .F. ) ;
#10106=DIRECTION ( 'NONE',  ( 0.000000000000000000, -2.891205793294679017E-15, -1.000000000000000000 ) ) ;
#10134=DIRECTION ( 'NONE',  ( 0.000000000000000000, 6.513401669715868659E-16, -1.000000000000000000 ) ) ;
#10148=DIRECTION ( 'NONE',  ( 0.000000000000000000, 4.336808689942017736E-16, -1.000000000000000000 ) ) ;
#10163=CARTESIAN_POINT ( 'NONE',  ( -3.476613658449256850, 7.159503395827455984E-16, 58.08258929006088067 ) ) ;
#10189=CYLINDRICAL_SURFACE ( 'NONE', #3691, 0.5999999999999998668 ) ;
#10190=EDGE_CURVE ( 'NONE', #13165, #11131, #10701, .T. ) ;
#10216=CIRCLE ( 'NONE', #5284, 0.5999999999999998668 ) ;
#10217=AXIS2_PLACEMENT_3D ( 'NONE', #3881, #5997, #13196 ) ;
#10218=ORIENTED_EDGE ( 'NONE', *, *, #5864, .F. ) ;
#10237=EDGE_LOOP ( 'NONE', ( #7545, #5743, #12750, #8764 ) ) ;
#10248=CARTESIAN_POINT ( 'NONE',  ( 12.65003830372715932, -3.992893622343521672E-16, 51.46292981703266634 ) ) ;
#10255=VECTOR ( 'NONE', #13398, 999.9999999999998863 ) ;
#10278=EDGE_CURVE ( 'NONE', #3437, #12431, #9257, .T. ) ;
#10285=VECTOR ( 'NONE', #10970, 1000.000000000000000 ) ;
#10289=AXIS2_PLACEMENT_3D ( 'NONE', #14526, #9713, #8633 ) ;
#10298=ORIENTED_EDGE ( 'NONE', *, *, #15107, .T. ) ;
#10304=CIRCLE ( 'NONE', #13267, 4.000000000000004441 ) ;
#10322=CARTESIAN_POINT ( 'NONE',  ( -23.31553094873632759, 2.149910154642043551E-15, 56.34690893053225125 ) ) ;
#10323=VECTOR ( 'NONE', #4450, 1000.000000000000000 ) ;
#10332=ORIENTED_EDGE ( 'NONE', *, *, #859, .F. ) ;
#10335=ORIENTED_EDGE ( 'NONE', *, *, #13014, .F. ) ;
#10339=ORIENTED_EDGE ( 'NONE', *, *, #13341, .F. ) ;
#10344=LINE ( 'NONE', #3214, #537 ) ;
#10351=CARTESIAN_POINT ( 'NONE',  ( 17.12895037488186389, -3.654606557864051197, 0.2687305842673423095 ) ) ;
#10354=CARTESIAN_POINT ( 'NONE',  ( 21.98164641901421135, -2.908542394189813650E-07, -0.3335879563140091153 ) ) ;
#10356=ORIENTED_EDGE ( 'NONE', *, *, #14820, .F. ) ;
#10360=DIRECTION ( 'NONE',  ( -0.08715574274766167695, 0.000000000000000000, 0.9961946980917453232 ) ) ;
#10362=DIRECTION ( 'NONE',  ( 1.000000000000000000, 0.000000000000000000, -0.000000000000000000 ) ) ;
#10369=EDGE_LOOP ( 'NONE', ( #12619, #1337, #14562, #9684 ) ) ;
#10383=CARTESIAN_POINT ( 'NONE',  ( 17.12895037488186389, -12.00000029085424025, 0.2687305842673423095 ) ) ;
#10393=FACE_OUTER_BOUND ( 'NONE', #4507, .T. ) ;
#10400=CARTESIAN_POINT ( 'NONE',  ( 16.99691247867024657, 3.529302617095105621, 1.266532794505838000 ) ) ;
#10424=CIRCLE ( 'NONE', #4491, 0.6000000000000000888 ) ;
#10432=CARTESIAN_POINT ( 'NONE',  ( 21.98164641901421135, 11.39999970914575833, -0.3335879563140091153 ) ) ;
#10435=( NAMED_UNIT ( * ) SI_UNIT ( $, .STERADIAN. ) SOLID_ANGLE_UNIT ( ) );
#10455=AXIS2_PLACEMENT_3D ( 'NONE', #2221, #6963, #11687 ) ;
#10456=DIRECTION ( 'NONE',  ( -0.08715574274766162144, 0.000000000000000000, 0.9961946980917453232 ) ) ;
#10458=DIRECTION ( 'NONE',  ( -0.9961946980917452121, 7.200509705930738460E-17, -0.08715574274766156593 ) ) ;
#10469=ORIENTED_EDGE ( 'NONE', *, *, #1047, .T. ) ;
#10476=CIRCLE ( 'NONE', #3800, 2.399999999999999467 ) ;
#10482=DIRECTION ( 'NONE',  ( 0.08715574274766037244, -0.000000000000000000, -0.9961946980917454342 ) ) ;
#10483=CARTESIAN_POINT ( 'NONE',  ( 21.98164641901421135, -12.00000029085423314, -14.73358795631400575 ) ) ;
#10485=DIRECTION ( 'NONE',  ( 0.000000000000000000, -1.000000000000000000, 0.000000000000000000 ) ) ;
#10491=AXIS2_PLACEMENT_3D ( 'NONE', #8431, #9432, #2618 ) ;
#10501=ORIENTED_EDGE ( 'NONE', *, *, #10278, .F. ) ;
#10502=CARTESIAN_POINT ( 'NONE',  ( 17.21626540049105003, -12.00000029085423670, -12.20299797093198535 ) ) ;
#10515=LINE ( 'NONE', #5811, #305 ) ;
#10517=ADVANCED_FACE ( 'NONE', ( #7453 ), #9673, .T. ) ;
#10525=ORIENTED_EDGE ( 'NONE', *, *, #13317, .F. ) ;
#10528=ORIENTED_EDGE ( 'NONE', *, *, #3225, .T. ) ;
#10536=CARTESIAN_POINT ( 'NONE',  ( 10.10406781373725771, -11.00000029085428110, 69.08979243323354069 ) ) ;
#10541=EDGE_CURVE ( 'NONE', #14951, #1333, #2782, .T. ) ;
#10562=CARTESIAN_POINT ( 'NONE',  ( 1.581646419014215654, -11.75147215343038987, 0.2664120436859910290 ) ) ;
#10579=DIRECTION ( 'NONE',  ( 0.000000000000000000, -0.1240337885538713436, 0.9922779949676268085 ) ) ;
#10580=CARTESIAN_POINT ( 'NONE',  ( -9.503456061879928640, -12.00000029085427222, 69.60114695342350899 ) ) ;
#10588=MANIFOLD_SOLID_BREP ( 'Cut-Extrude4', #6072 ) ;
#10615=CARTESIAN_POINT ( 'NONE',  ( 10.10406781373725948, 11.99999970914572955, 69.08979243323354069 ) ) ;
#10627=ORIENTED_EDGE ( 'NONE', *, *, #3844, .F. ) ;
#10646=DIRECTION ( 'NONE',  ( 0.9961946980917452121, -3.779777825264104572E-17, 0.08715574274766174634 ) ) ;
#10660=ORIENTED_EDGE ( 'NONE', *, *, #13897, .F. ) ;
#10664=ADVANCED_FACE ( 'NONE', ( #5900, #9358 ), #906, .F. ) ;
#10666=EDGE_CURVE ( 'NONE', #9779, #4992, #10515, .T. ) ;
#10689=ADVANCED_BREP_SHAPE_REPRESENTATION ( '', ( #10716, #10588, #285 ), #2528 ) ;
#10690=AXIS2_PLACEMENT_3D ( 'NONE', #13752, #712, #3123 ) ;
#10701=CIRCLE ( 'NONE', #7970, 0.5999999999999998668 ) ;
#10704=ORIENTED_EDGE ( 'NONE', *, *, #3096, .F. ) ;
#10712=CARTESIAN_POINT ( 'NONE',  ( -8.108964177917338034, 5.861171052203404620E-16, 53.66203178395558382 ) ) ;
#10716=MANIFOLD_SOLID_BREP ( 'Boss-Extrude6', #13256 ) ;
#10724=CARTESIAN_POINT ( 'NONE',  ( 17.00398511370262256, -11.48933746301553960, 0.2918493266781312379 ) ) ;
#10725=EDGE_CURVE ( 'NONE', #12773, #8985, #559, .T. ) ;
#10754=CARTESIAN_POINT ( 'NONE',  ( 16.99691247867024657, -3.779330867977714892, 1.266532794505838000 ) ) ;
#10768=AXIS2_PLACEMENT_3D ( 'NONE', #9166, #5630, #3206 ) ;
#10784=CYLINDRICAL_SURFACE ( 'NONE', #7826, 0.5999999999999998668 ) ;
#10788=ORIENTED_EDGE ( 'NONE', *, *, #6158, .T. ) ;
#10793=EDGE_LOOP ( 'NONE', ( #5150, #9784, #9808, #8019 ) ) ;
#10794=AXIS2_PLACEMENT_3D ( 'NONE', #8501, #6048, #13015 ) ;
#10801=CARTESIAN_POINT ( 'NONE',  ( 1.634139617129772404, -12.00000029085424025, -0.3335879563140197179 ) ) ;
#10810=CARTESIAN_POINT ( 'NONE',  ( 17.18164641901421419, -12.00000029085424380, 0.8664120436859873431 ) ) ;
#10823=DIRECTION ( 'NONE',  ( -0.000000000000000000, -4.336808689942017736E-16, 1.000000000000000000 ) ) ;
#10824=ORIENTED_EDGE ( 'NONE', *, *, #9712, .T. ) ;
#10827=CARTESIAN_POINT ( 'NONE',  ( 16.21690705545749367, 11.99999970914575798, 0.2773483677299301564 ) ) ;
#10828=AXIS2_PLACEMENT_3D ( 'NONE', #1231, #2467, #2238 ) ;
#10840=DIRECTION ( 'NONE',  ( 0.08715574274766176022, 4.320305823558445788E-16, -0.9961946980917453232 ) ) ;
#10863=CARTESIAN_POINT ( 'NONE',  ( -12.81835358098578403, -12.00000029085423670, -11.73358795631400930 ) ) ;
#10874=CYLINDRICAL_SURFACE ( 'NONE', #787, 4.000000000000004441 ) ;
#10875=EDGE_CURVE ( 'NONE', #6249, #1167, #8739, .T. ) ;
#10878=CARTESIAN_POINT ( 'NONE',  ( 22.58164641901421632, 11.99999970914576330, -11.73358795631400397 ) ) ;
#10884=CARTESIAN_POINT ( 'NONE',  ( 17.21739630941073429, 3.678509596725633823, 0.07286771090926232042 ) ) ;
#10890=ORIENTED_EDGE ( 'NONE', *, *, #12853, .T. ) ;
#10906=APPLICATION_CONTEXT ( 'automotive_design' ) ;
#10914=DIRECTION ( 'NONE',  ( 0.08715574274766176022, 0.000000000000000000, -0.9961946980917453232 ) ) ;
#10922=ORIENTED_EDGE ( 'NONE', *, *, #3917, .T. ) ;
#10926=CIRCLE ( 'NONE', #758, 4.000000000000004441 ) ;
#10931=SPHERICAL_SURFACE ( 'NONE', #15238, 0.6000000000000000888 ) ;
#10933=ORIENTED_EDGE ( 'NONE', *, *, #15200, .F. ) ;
#10937=CIRCLE ( 'NONE', #13425, 4.000000000000004441 ) ;
#10939=ORIENTED_EDGE ( 'NONE', *, *, #7417, .T. ) ;
#10941=ADVANCED_FACE ( 'NONE', ( #4003, #7513 ), #1605, .T. ) ;
#10942=CARTESIAN_POINT ( 'NONE',  ( 21.98164641901421135, -12.00000029085424025, -8.183940086454239093 ) ) ;
#10946=DIRECTION ( 'NONE',  ( 0.9833652781161342782, 0.000000000000000000, 0.1816390095645149805 ) ) ;
#10958=AXIS2_PLACEMENT_3D ( 'NONE', #1374, #1454, #10914 ) ;
#10965=EDGE_CURVE ( 'NONE', #2847, #6145, #3505, .T. ) ;
#10970=DIRECTION ( 'NONE',  ( -1.000000000000000000, 0.000000000000000000, 0.000000000000000000 ) ) ;
#10974=DIRECTION ( 'NONE',  ( 1.000000000000000000, 0.000000000000000000, -0.000000000000000000 ) ) ;
#10989=CARTESIAN_POINT ( 'NONE',  ( -22.61828500675503761, 1.660051434983101380E-15, 48.37735134579827445 ) ) ;
#10991=LINE ( 'NONE', #2760, #9312 ) ;
#11019=CARTESIAN_POINT ( 'NONE',  ( 10.10406781373725771, 10.99999970914572778, 69.08979243323354069 ) ) ;
#11025=CARTESIAN_POINT ( 'NONE',  ( -12.81835358098578403, -12.50000029085423847, -8.775548064764199907 ) ) ;
#11030=CARTESIAN_POINT ( 'NONE',  ( 17.12895037488186389, 3.654026927208769315, 0.2687305842673423095 ) ) ;
#11046=TOROIDAL_SURFACE ( 'NONE', #13034, 1.200000000000000178, 0.6000000000000000888 ) ;
#11066=AXIS2_PLACEMENT_3D ( 'NONE', #13937, #8043, #6898 ) ;
#11068=CARTESIAN_POINT ( 'NONE',  ( 21.98164641901421135, 11.99999970914576330, -11.73358795631400753 ) ) ;
#11077=CYLINDRICAL_SURFACE ( 'NONE', #12790, 0.9999999999999956701 ) ;
#11083=AXIS2_PLACEMENT_3D ( 'NONE', #10810, #175, #9701 ) ;
#11101=EDGE_CURVE ( 'NONE', #11742, #2988, #14439, .T. ) ;
#11102=CIRCLE ( 'NONE', #4409, 0.5999999999999998668 ) ;
#11125=CARTESIAN_POINT ( 'NONE',  ( 10.10045295220800554, -85.69524470659703752, 70.08978589960021566 ) ) ;
#11131=VERTEX_POINT ( 'NONE', #10483 ) ;
#11142=CARTESIAN_POINT ( 'NONE',  ( -13.41835358098578723, 11.39999970914575833, 0.2664120436859911956 ) ) ;
#11162=DIRECTION ( 'NONE',  ( 0.000000000000000000, 1.000000000000000000, 0.000000000000000000 ) ) ;
#11163=VERTEX_POINT ( 'NONE', #9859 ) ;
#11174=DIRECTION ( 'NONE',  ( 1.000000000000000000, 0.000000000000000000, 0.000000000000000000 ) ) ;
#11182=ORIENTED_EDGE ( 'NONE', *, *, #3257, .F. ) ;
#11199=CARTESIAN_POINT ( 'NONE',  ( 22.58164641901421632, 11.39999970914576188, -8.183940086454237317 ) ) ;
#11202=ORIENTED_EDGE ( 'NONE', *, *, #5804, .T. ) ;
#11208=DIRECTION ( 'NONE',  ( -0.9999934663667179313, 1.567696289299852414E-18, -0.003614861529252313445 ) ) ;
#11217=VECTOR ( 'NONE', #9446, 1000.000000000000114 ) ;
#11223=CARTESIAN_POINT ( 'NONE',  ( 11.02372356922131758, 11.99999970914572955, 69.09311688316493871 ) ) ;
#11254=CARTESIAN_POINT ( 'NONE',  ( 21.98164641901421135, 11.39999970914576011, -8.183940086454237317 ) ) ;
#11256=EDGE_CURVE ( 'NONE', #14071, #8700, #15042, .T. ) ;
#11258=CARTESIAN_POINT ( 'NONE',  ( -9.503456061879928640, -12.00000029085427222, 69.60114695342350899 ) ) ;
#11263=SHAPE_REPRESENTATION ( 'Sliding Jaws', ( #285 ), #2528 ) ;
#11264=EDGE_LOOP ( 'NONE', ( #9517, #5678, #6567, #12261 ) ) ;
#11266=ORIENTED_EDGE ( 'NONE', *, *, #4909, .F. ) ;
#11280=DIRECTION ( 'NONE',  ( 0.000000000000000000, 0.000000000000000000, -1.000000000000000000 ) ) ;
#11295=FACE_OUTER_BOUND ( 'NONE', #13944, .T. ) ;
#11298=SPHERICAL_SURFACE ( 'NONE', #7000, 0.6000000000000000888 ) ;
#11310=SURFACE_STYLE_FILL_AREA ( #6598 ) ;
#11311=DIRECTION ( 'NONE',  ( 0.000000000000000000, 1.000000000000000000, 0.000000000000000000 ) ) ;
#11319=EDGE_LOOP ( 'NONE', ( #1238, #3366, #5690, #14577 ) ) ;
#11320=ORIENTED_EDGE ( 'NONE', *, *, #9886, .F. ) ;
#11326=EDGE_CURVE ( 'NONE', #13856, #12032, #4355, .T. ) ;
#11338=ORIENTED_EDGE ( 'NONE', *, *, #4, .T. ) ;
#11339=DIRECTION ( 'NONE',  ( 1.000000000000000000, -0.000000000000000000, 0.000000000000000000 ) ) ;
#11340=ORIENTED_EDGE ( 'NONE', *, *, #12258, .F. ) ;
#11342=VERTEX_POINT ( 'NONE', #9002 ) ;
#11350=CARTESIAN_POINT ( 'NONE',  ( -4.522482571421201136, -12.00000029085427222, 70.03692566716181034 ) ) ;
#11362=ORIENTED_EDGE ( 'NONE', *, *, #2125, .F. ) ;
#11363=B_SPLINE_CURVE_WITH_KNOTS ( 'NONE', 3,
 ( #12324, #1833, #669, #4243 ),
 .UNSPECIFIED., .F., .F.,
 ( 4, 4 ),
 ( 0.000000000000000000, 0.0004098597307629696612 ),
 .UNSPECIFIED. ) ;
#11376=ORIENTED_EDGE ( 'NONE', *, *, #5844, .F. ) ;
#11380=DIRECTION ( 'NONE',  ( 0.000000000000000000, -1.000000000000000000, -4.336808689942017736E-16 ) ) ;
#11381=LINE ( 'NONE', #7963, #3358 ) ;
#11386=EDGE_CURVE ( 'NONE', #5234, #5837, #5836, .T. ) ;
#11402=EDGE_CURVE ( 'NONE', #4340, #15166, #4960, .T. ) ;
#11412=PLANE ( 'NONE',  #4767 ) ;
#11420=AXIS2_PLACEMENT_3D ( 'NONE', #12069, #1508, #8489 ) ;
#11454=EDGE_LOOP ( 'NONE', ( #5982, #12868 ) ) ;
#11464=CARTESIAN_POINT ( 'NONE',  ( 17.12895037488186389, 11.13833052492975106, 0.2687305842673423095 ) ) ;
#11466=ORIENTED_EDGE ( 'NONE', *, *, #11496, .T. ) ;
#11484=CARTESIAN_POINT ( 'NONE',  ( 14.79833345856040694, -1.094824204497501265E-15, 26.90780383552089106 ) ) ;
#11496=EDGE_CURVE ( 'NONE', #14868, #7121, #8266, .T. ) ;
#11503=DIRECTION ( 'NONE',  ( 0.000000000000000000, -1.000000000000000000, -4.336808689942017736E-16 ) ) ;
#11505=CYLINDRICAL_SURFACE ( 'NONE', #15279, 0.5999999999999998668 ) ;
#11507=VECTOR ( 'NONE', #7693, 999.9999999999998863 ) ;
#11518=CARTESIAN_POINT ( 'NONE',  ( 22.58164641901421632, 11.99999970914576863, -56.77834603255778489 ) ) ;
#11545=VERTEX_POINT ( 'NONE', #223 ) ;
#11551=VECTOR ( 'NONE', #13333, 1000.000000000000114 ) ;
#11555=LINE ( 'NONE', #3177, #7300 ) ;
#11556=VECTOR ( 'NONE', #14974, 1000.000000000000000 ) ;
#11561=DIRECTION ( 'NONE',  ( 0.000000000000000000, -4.336808689942017736E-16, 1.000000000000000000 ) ) ;
#11567=VECTOR ( 'NONE', #2398, 1000.000000000000114 ) ;
#11575=AXIS2_PLACEMENT_3D ( 'NONE', #11766, #14529, #11614 ) ;
#11583=ORIENTED_EDGE ( 'NONE', *, *, #5085, .F. ) ;
#11589=CARTESIAN_POINT ( 'NONE',  ( 17.18164641901421419, -12.00000029085424202, -0.3335879563140091153 ) ) ;
#11598=LINE ( 'NONE', #4387, #3296 ) ;
#11602=CARTESIAN_POINT ( 'NONE',  ( 17.16405274069114739, -3.654316742536410256, 0.2664120436859874763 ) ) ;
#11612=EDGE_CURVE ( 'NONE', #2233, #4222, #8448, .T. ) ;
#11614=DIRECTION ( 'NONE',  ( 0.000000000000000000, 0.000000000000000000, -1.000000000000000000 ) ) ;
#11620=ADVANCED_FACE ( 'NONE', ( #381 ), #1475, .T. ) ;
#11628=ORIENTED_EDGE ( 'NONE', *, *, #13708, .F. ) ;
#11634=CARTESIAN_POINT ( 'NONE',  ( 24.12375314681476368, -1.228611132858002289E-15, 52.46674979433200292 ) ) ;
#11670=DIRECTION ( 'NONE',  ( 0.000000000000000000, 0.000000000000000000, -1.000000000000000000 ) ) ;
#11671=ORIENTED_EDGE ( 'NONE', *, *, #8316, .T. ) ;
#11686=LINE ( 'NONE', #13102, #12611 ) ;
#11687=DIRECTION ( 'NONE',  ( 0.000000000000000000, 0.000000000000000000, -1.000000000000000000 ) ) ;
#11688=CARTESIAN_POINT ( 'NONE',  ( -12.81835358098578403, -12.60000029085423812, -8.183940086454239093 ) ) ;
#11694=EDGE_LOOP ( 'NONE', ( #9400, #1108, #69, #648 ) ) ;
#11710=MECHANICAL_DESIGN_GEOMETRIC_PRESENTATION_REPRESENTATION('',(#4527),#12459);
#11717=CARTESIAN_POINT ( 'NONE',  ( -4.435020996998820131, -12.00000029085427045, 69.03723529703216855 ) ) ;
#11735=CARTESIAN_POINT ( 'NONE',  ( 1.603389813606017622, -12.00000029085424735, 0.01788390626212849749 ) ) ;
#11736=CARTESIAN_POINT ( 'NONE',  ( 11.02010870769206541, -85.69524470659703752, 70.09311034953161368 ) ) ;
#11742=VERTEX_POINT ( 'NONE', #6601 ) ;
#11747=VERTEX_POINT ( 'NONE', #5586 ) ;
#11763=AXIS2_PLACEMENT_3D ( 'NONE', #2374, #7127, #5019 ) ;
#11766=CARTESIAN_POINT ( 'NONE',  ( 22.58164641901421632, -12.60000029085423812, -8.183940086454239093 ) ) ;
#11767=DIRECTION ( 'NONE',  ( 0.000000000000000000, 0.000000000000000000, -1.000000000000000000 ) ) ;
#11774=EDGE_CURVE ( 'NONE', #5737, #2678, #9283, .T. ) ;
#11780=ADVANCED_FACE ( 'NONE', ( #7612 ), #3015, .F. ) ;
#11781=ORIENTED_EDGE ( 'NONE', *, *, #2772, .F. ) ;
#11803=EDGE_LOOP ( 'NONE', ( #3725, #4468, #12009, #3041 ) ) ;
#11811=DIRECTION ( 'NONE',  ( 1.000000000000000000, -0.000000000000000000, 0.000000000000000000 ) ) ;
#11822=AXIS2_PLACEMENT_3D ( 'NONE', #5569, #10047, #1123 ) ;
#11824=AXIS2_PLACEMENT_3D ( 'NONE', #8521, #13573, #9669 ) ;
#11829=DIRECTION ( 'NONE',  ( -1.000000000000000000, 1.734723475976808672E-15, 5.828670879282076886E-13 ) ) ;
#11852=EDGE_LOOP ( 'NONE', ( #12572, #10824, #6827, #1456 ) ) ;
#11859=VERTEX_POINT ( 'NONE', #4717 ) ;
#11873=DIRECTION ( 'NONE',  ( -0.000000000000000000, 4.336808689942017736E-16, -1.000000000000000000 ) ) ;
#11886=DIRECTION ( 'NONE',  ( 0.000000000000000000, -1.000000000000000000, -4.336808689942017736E-16 ) ) ;
#11892=DIRECTION ( 'NONE',  ( -0.9961946980917453232, 7.200509705930738460E-17, -0.08715574274766157981 ) ) ;
#11896=DIRECTION ( 'NONE',  ( 0.000000000000000000, 0.000000000000000000, 1.000000000000000000 ) ) ;
#11899=ORIENTED_EDGE ( 'NONE', *, *, #151, .F. ) ;
#11907=FACE_OUTER_BOUND ( 'NONE', #7194, .T. ) ;
#11927=CIRCLE ( 'NONE', #3246, 0.5999999999999998668 ) ;
#11928=VERTEX_POINT ( 'NONE', #50 ) ;
#11936=AXIS2_PLACEMENT_3D ( 'NONE', #2129, #2274, #3290 ) ;
#11947=ORIENTED_EDGE ( 'NONE', *, *, #13519, .T. ) ;
#11961=DIRECTION ( 'NONE',  ( 0.000000000000000000, -0.1666666666666656582, 0.9860132971832695770 ) ) ;
#11968=DIRECTION ( 'NONE',  ( 1.000000000000000000, -0.000000000000000000, 0.000000000000000000 ) ) ;
#11984=DIRECTION ( 'NONE',  ( -1.000000000000000000, 0.000000000000000000, -0.000000000000000000 ) ) ;
#11992=AXIS2_PLACEMENT_3D ( 'NONE', #7189, #9263, #11670 ) ;
#11995=ORIENTED_EDGE ( 'NONE', *, *, #4575, .T. ) ;
#12003=DIRECTION ( 'NONE',  ( -0.000000000000000000, 0.9922779949676268085, 0.1240337885538713436 ) ) ;
#12004=ADVANCED_FACE ( 'NONE', ( #2614, #3701, #8429 ), #12233, .T. ) ;
#12009=ORIENTED_EDGE ( 'NONE', *, *, #8763, .T. ) ;
#12012=CIRCLE ( 'NONE', #10768, 2.399999999999999467 ) ;
#12027=CARTESIAN_POINT ( 'NONE',  ( 17.12895037488186389, -11.00000029085424913, 0.2687305842673423095 ) ) ;
#12032=VERTEX_POINT ( 'NONE', #13404 ) ;
#12054=CARTESIAN_POINT ( 'NONE',  ( 16.82703061321707949, -11.72093437952781336, 0.2761868948537983814 ) ) ;
#12057=CARTESIAN_POINT ( 'NONE',  ( -4.435020996998820131, -12.00000029085427045, 69.03723529703216855 ) ) ;
#12066=CARTESIAN_POINT ( 'NONE',  ( 22.58164641901421632, 11.39999970914575833, -0.3335879563140091153 ) ) ;
#12069=CARTESIAN_POINT ( 'NONE',  ( -12.81835358098578759, 11.39999970914576188, -8.183940086454237317 ) ) ;
#12072=CARTESIAN_POINT ( 'NONE',  ( -13.41835358098578723, 11.39999970914575833, -0.3335879563140091153 ) ) ;
#12075=VERTEX_POINT ( 'NONE', #1752 ) ;
#12081=LINE ( 'NONE', #3247, #5599 ) ;
#12090=ORIENTED_EDGE ( 'NONE', *, *, #13708, .T. ) ;
#12098=ADVANCED_FACE ( 'NONE', ( #2928 ), #13481, .T. ) ;
#12111=ORIENTED_EDGE ( 'NONE', *, *, #6979, .F. ) ;
#12124=CARTESIAN_POINT ( 'NONE',  ( 12.30141533273650900, -8.891480818932939924E-16, 55.44770860939965473 ) ) ;
#12128=EDGE_LOOP ( 'NONE', ( #410, #6081, #534, #155, #798, #6969, #7688, #5868, #4032 ) ) ;
#12140=LINE ( 'NONE', #8638, #3243 ) ;
#12143=ORIENTED_EDGE ( 'NONE', *, *, #5824, .F. ) ;
#12154=LINE ( 'NONE', #7361, #11551 ) ;
#12166=FACE_OUTER_BOUND ( 'NONE', #8839, .T. ) ;
#12175=VERTEX_POINT ( 'NONE', #3155 ) ;
#12180=LINE ( 'NONE', #12343, #11507 ) ;
#12183=ADVANCED_FACE ( 'NONE', ( #13565 ), #11298, .T. ) ;
#12188=CARTESIAN_POINT ( 'NONE',  ( 22.58164641901421632, -12.00000029085423670, -11.73358795631401463 ) ) ;
#12196=ORIENTED_EDGE ( 'NONE', *, *, #12238, .T. ) ;
#12215=DIRECTION ( 'NONE',  ( 0.000000000000000000, 0.000000000000000000, -1.000000000000000000 ) ) ;
#12219=FACE_OUTER_BOUND ( 'NONE', #4432, .T. ) ;
#12222=VECTOR ( 'NONE', #13885, 1000.000000000000000 ) ;
#12233=PLANE ( 'NONE',  #10958 ) ;
#12238=EDGE_CURVE ( 'NONE', #6473, #14750, #9848, .T. ) ;
#12246=CYLINDRICAL_SURFACE ( 'NONE', #11824, 4.000000000000000888 ) ;
#12249=DIRECTION ( 'NONE',  ( 1.517216463963902273E-16, -1.000000000000000000, -1.734186353771755353E-15 ) ) ;
#12258=EDGE_CURVE ( 'NONE', #7132, #6631, #13201, .T. ) ;
#12259=EDGE_LOOP ( 'NONE', ( #2229, #12967, #13006, #3197 ) ) ;
#12261=ORIENTED_EDGE ( 'NONE', *, *, #9338, .F. ) ;
#12277=CARTESIAN_POINT ( 'NONE',  ( -13.41835358098578723, 11.75147157172190049, 0.2664120436859908625 ) ) ;
#12296=AXIS2_PLACEMENT_3D ( 'NONE', #14388, #8507, #3932 ) ;
#12298=DIRECTION ( 'NONE',  ( 0.000000000000000000, 0.000000000000000000, -1.000000000000000000 ) ) ;
#12312=DIRECTION ( 'NONE',  ( 0.08715574274766176022, 0.000000000000000000, -0.9961946980917453232 ) ) ;
#12316=AXIS2_PLACEMENT_3D ( 'NONE', #697, #8923, #925 ) ;
#12324=CARTESIAN_POINT ( 'NONE',  ( 17.12895037488186389, -11.00000029085424913, 0.2687305842673423095 ) ) ;
#12334=DIRECTION ( 'NONE',  ( -1.000000000000000000, -0.000000000000000000, -0.000000000000000000 ) ) ;
#12343=CARTESIAN_POINT ( 'NONE',  ( 1.634139617129772404, 11.99999970914575798, -0.3335879563140092818 ) ) ;
#12346=VECTOR ( 'NONE', #999, 1000.000000000000000 ) ;
#12361=CIRCLE ( 'NONE', #14088, 3.000000000000000888 ) ;
#12369=FACE_OUTER_BOUND ( 'NONE', #12906, .T. ) ;
#12381=DIRECTION ( 'NONE',  ( 0.000000000000000000, 4.336808689942017736E-16, -1.000000000000000000 ) ) ;
#12391=CARTESIAN_POINT ( 'NONE',  ( 21.98164641901421135, 11.39999970914575833, -0.3335879563140091153 ) ) ;
#12392=CARTESIAN_POINT ( 'NONE',  ( 22.58164641901421632, -2.908542394189813650E-07, -11.73358795631400930 ) ) ;
#12397=ORIENTED_EDGE ( 'NONE', *, *, #9335, .F. ) ;
#12401=EDGE_CURVE ( 'NONE', #11742, #5737, #1170, .T. ) ;
#12406=FILL_AREA_STYLE_COLOUR ( '', #6032 ) ;
#12421=CARTESIAN_POINT ( 'NONE',  ( 10.10406781373725771, -12.00000029085427222, 69.08979243323352648 ) ) ;
#12426=DIRECTION ( 'NONE',  ( 0.000000000000000000, -4.336808689942017736E-16, 1.000000000000000000 ) ) ;
#12431=VERTEX_POINT ( 'NONE', #2108 ) ;
#12437=AXIS2_PLACEMENT_3D ( 'NONE', #11068, #5176, #3145 ) ;
#12459=( GEOMETRIC_REPRESENTATION_CONTEXT ( 3 ) GLOBAL_UNCERTAINTY_ASSIGNED_CONTEXT ( ( #324 ) ) GLOBAL_UNIT_ASSIGNED_CONTEXT ( ( #9126, #9427, #10435 ) ) REPRESENTATION_CONTEXT ( 'NONE', 'WORKASPACE' ) );
#12465=VECTOR ( 'NONE', #9887, 1000.000000000000114 ) ;
#12472=EDGE_CURVE ( 'NONE', #6145, #12075, #15124, .T. ) ;
#12474=ORIENTED_EDGE ( 'NONE', *, *, #7925, .F. ) ;
#12491=VERTEX_POINT ( 'NONE', #1176 ) ;
#12527=ORIENTED_EDGE ( 'NONE', *, *, #12938, .F. ) ;
#12530=ORIENTED_EDGE ( 'NONE', *, *, #12938, .T. ) ;
#12541=EDGE_CURVE ( 'NONE', #411, #14750, #4678, .T. ) ;
#12549=AXIS2_PLACEMENT_3D ( 'NONE', #6410, #1728, #1504 ) ;
#12560=ADVANCED_FACE ( 'NONE', ( #9541 ), #7550, .F. ) ;
#12561=PLANE ( 'NONE',  #8635 ) ;
#12562=DIRECTION ( 'NONE',  ( 1.000000000000000000, 0.000000000000000000, 0.000000000000000000 ) ) ;
#12572=ORIENTED_EDGE ( 'NONE', *, *, #6253, .F. ) ;
#12580=LINE ( 'NONE', #4199, #9571 ) ;
#12588=ORIENTED_EDGE ( 'NONE', *, *, #1847, .F. ) ;
#12591=VERTEX_POINT ( 'NONE', #11025 ) ;
#12595=ADVANCED_FACE ( 'NONE', ( #4979 ), #14506, .T. ) ;
#12607=EDGE_LOOP ( 'NONE', ( #5967, #13585, #6077, #10660, #12995 ) ) ;
#12611=VECTOR ( 'NONE', #5899, 1000.000000000000000 ) ;
#12614=DIRECTION ( 'NONE',  ( 0.000000000000000000, 0.000000000000000000, -1.000000000000000000 ) ) ;
#12616=FACE_OUTER_BOUND ( 'NONE', #7690, .T. ) ;
#12619=ORIENTED_EDGE ( 'NONE', *, *, #13799, .F. ) ;
#12625=CARTESIAN_POINT ( 'NONE',  ( 17.23697745638123280, -3.616872831399570831, -0.03314156585704653574 ) ) ;
#12626=CARTESIAN_POINT ( 'NONE',  ( -4.522482571421200248, 10.99999970914572422, 70.03692566716178192 ) ) ;
#12632=ORIENTED_EDGE ( 'NONE', *, *, #13061, .F. ) ;
#12654=ORIENTED_EDGE ( 'NONE', *, *, #6158, .F. ) ;
#12661=DIRECTION ( 'NONE',  ( 0.000000000000000000, 0.000000000000000000, -1.000000000000000000 ) ) ;
#12682=CARTESIAN_POINT ( 'NONE',  ( 10.10406781373725771, -11.00000029085427045, 69.08979243323354069 ) ) ;
#12724=CARTESIAN_POINT ( 'NONE',  ( 17.12895037488186389, 3.654026927208769315, 0.2687305842673423095 ) ) ;
#12728=EDGE_LOOP ( 'NONE', ( #2890, #1358, #707, #793, #4416, #2200 ) ) ;
#12739=CARTESIAN_POINT ( 'NONE',  ( 17.12895037488186389, -12.00000029085424025, 0.2687305842673423095 ) ) ;
#12750=ORIENTED_EDGE ( 'NONE', *, *, #5092, .T. ) ;
#12760=EDGE_CURVE ( 'NONE', #1550, #6145, #10216, .T. ) ;
#12762=CARTESIAN_POINT ( 'NONE',  ( -13.41835358098578723, 12.59999970914575940, -8.183940086454237317 ) ) ;
#12765=CARTESIAN_POINT ( 'NONE',  ( -12.81835358098578403, 11.39999970914576366, -11.73358795631400397 ) ) ;
#12771=CYLINDRICAL_SURFACE ( 'NONE', #13280, 0.6000000000000000888 ) ;
#12773=VERTEX_POINT ( 'NONE', #8773 ) ;
#12778=VECTOR ( 'NONE', #241, 1000.000000000000000 ) ;
#12790=AXIS2_PLACEMENT_3D ( 'NONE', #4005, #513, #2692 ) ;
#12798=DIRECTION ( 'NONE',  ( 0.003614861529251474706, 0.000000000000000000, -0.9999934663667180423 ) ) ;
#12800=CYLINDRICAL_SURFACE ( 'NONE', #3924, 0.5999999999999998668 ) ;
#12805=CARTESIAN_POINT ( 'NONE',  ( -12.81835358098578759, -12.00000029085424025, -8.733587956314007528 ) ) ;
#12829=CIRCLE ( 'NONE', #8120, 0.5999999999999999778 ) ;
#12837=ORIENTED_EDGE ( 'NONE', *, *, #2706, .T. ) ;
#12853=EDGE_CURVE ( 'NONE', #7763, #2194, #4729, .T. ) ;
#12868=ORIENTED_EDGE ( 'NONE', *, *, #4556, .F. ) ;
#12896=FACE_OUTER_BOUND ( 'NONE', #6529, .T. ) ;
#12906=EDGE_LOOP ( 'NONE', ( #9384, #227, #12397, #10339 ) ) ;
#12911=VECTOR ( 'NONE', #4471, 1000.000000000000000 ) ;
#12912=DIRECTION ( 'NONE',  ( -1.000000000000000000, 0.000000000000000000, -0.000000000000000000 ) ) ;
#12922=SHAPE_DEFINITION_REPRESENTATION ( #14743, #11263 ) ;
#12935=CARTESIAN_POINT ( 'NONE',  ( 21.98164641901421135, -12.00000029085424202, -0.3335879563140091153 ) ) ;
#12936=FILL_AREA_STYLE_COLOUR ( '', #1297 ) ;
#12938=EDGE_CURVE ( 'NONE', #1333, #6768, #15160, .T. ) ;
#12950=PRODUCT_DEFINITION_FORMATION_WITH_SPECIFIED_SOURCE ( 'ANY', '', #1739, .NOT_KNOWN. ) ;
#12959=AXIS2_PLACEMENT_3D ( 'NONE', #13351, #6223, #1473 ) ;
#12967=ORIENTED_EDGE ( 'NONE', *, *, #6703, .T. ) ;
#12971=ORIENTED_EDGE ( 'NONE', *, *, #6853, .T. ) ;
#12984=DIRECTION ( 'NONE',  ( 0.9999934663667179313, 0.000000000000000000, 0.003614861529252313445 ) ) ;
#12991=CARTESIAN_POINT ( 'NONE',  ( 17.18164641901421419, -12.00000029085424025, 0.8664120436859875651 ) ) ;
#12995=ORIENTED_EDGE ( 'NONE', *, *, #11774, .F. ) ;
#13006=ORIENTED_EDGE ( 'NONE', *, *, #13072, .T. ) ;
#13011=VECTOR ( 'NONE', #10458, 1000.000000000000114 ) ;
#13014=EDGE_CURVE ( 'NONE', #5785, #4566, #5178, .T. ) ;
#13015=DIRECTION ( 'NONE',  ( 0.000000000000000000, 0.000000000000000000, -1.000000000000000000 ) ) ;
#13026=ORIENTED_EDGE ( 'NONE', *, *, #11496, .F. ) ;
#13029=ORIENTED_EDGE ( 'NONE', *, *, #1242, .F. ) ;
#13034=AXIS2_PLACEMENT_3D ( 'NONE', #504, #2917, #12381 ) ;
#13049=FACE_OUTER_BOUND ( 'NONE', #10793, .T. ) ;
#13053=VERTEX_POINT ( 'NONE', #3928 ) ;
#13059=EDGE_CURVE ( 'NONE', #8152, #9489, #8651, .T. ) ;
#13061=EDGE_CURVE ( 'NONE', #4503, #2194, #13459, .T. ) ;
#13072=EDGE_CURVE ( 'NONE', #5033, #5785, #13560, .T. ) ;
#13076=EDGE_LOOP ( 'NONE', ( #1950, #6790, #4483, #8423 ) ) ;
#13086=LINE ( 'NONE', #3607, #4541 ) ;
#13093=EDGE_LOOP ( 'NONE', ( #6054, #1302, #2789, #5322, #10501, #14104 ) ) ;
#13102=CARTESIAN_POINT ( 'NONE',  ( 22.58164641901421632, -12.50000029085423847, -8.775548064764199907 ) ) ;
#13119=CARTESIAN_POINT ( 'NONE',  ( 21.98164641901421135, -12.60000029085423812, -8.183940086454239093 ) ) ;
#13134=CARTESIAN_POINT ( 'NONE',  ( 22.58164641901420921, -3.623250966006795970, 0.01788390626213397228 ) ) ;
#13139=DIRECTION ( 'NONE',  ( 0.000000000000000000, -4.336808689942017736E-16, 1.000000000000000000 ) ) ;
#13141=CARTESIAN_POINT ( 'NONE',  ( 16.58164641901421277, 11.39999970914575833, 0.2664120436859911956 ) ) ;
#13142=DIRECTION ( 'NONE',  ( 0.000000000000000000, 0.000000000000000000, -1.000000000000000000 ) ) ;
#13144=CARTESIAN_POINT ( 'NONE',  ( 16.95292505576233566, -11.57157634197346852, 0.2884589904497822932 ) ) ;
#13149=CARTESIAN_POINT ( 'NONE',  ( 15.14695642955105193, -1.094824204497501265E-15, 22.92302504315390621 ) ) ;
#13152=EDGE_CURVE ( 'NONE', #9494, #5961, #11598, .T. ) ;
#13165=VERTEX_POINT ( 'NONE', #9178 ) ;
#13189=LINE ( 'NONE', #4893, #4816 ) ;
#13196=DIRECTION ( 'NONE',  ( 0.000000000000000000, 0.000000000000000000, -1.000000000000000000 ) ) ;
#13201=CIRCLE ( 'NONE', #302, 0.9999999999999957812 ) ;
#13227=EDGE_CURVE ( 'NONE', #12491, #7325, #8261, .T. ) ;
#13239=CARTESIAN_POINT ( 'NONE',  ( 17.12895037488186389, 3.654026927208769315, 0.2687305842673423095 ) ) ;
#13242=ADVANCED_FACE ( 'NONE', ( #14777 ), #7808, .T. ) ;
#13249=CARTESIAN_POINT ( 'NONE',  ( 0.06617338034656250478, 5.102742169785384244E-16, 17.58834813908115180 ) ) ;
#13256=CLOSED_SHELL ( 'NONE', ( #2466, #1956, #7184, #14840, #4958, #8578, #296, #13353, #8637, #6705, #2973, #12560, #13789, #6574, #9317, #11620, #6033, #1471, #9009, #9419, #9607, #11780, #5619, #4703, #9246, #13503, #9159, #8257, #4983, #431, #4425, #4410, #39, #5080, #4674, #12183, #4303, #1805, #2042, #9189, #3853, #13974, #12004, #3677, #15303, #3440, #12595, #8679, #2594, #15308, #12098, #14037, #1004, #10517, #13242, #3146, #4786 ) ) ;
#13260=CARTESIAN_POINT ( 'NONE',  ( 22.58164641901421632, 11.99999970914576686, -14.73358795631400575 ) ) ;
#13266=CARTESIAN_POINT ( 'NONE',  ( -4.522482571421200248, -85.69524470659703752, 70.03692566716173928 ) ) ;
#13267=AXIS2_PLACEMENT_3D ( 'NONE', #10712, #9235, #1013 ) ;
#13270=AXIS2_PLACEMENT_3D ( 'NONE', #13520, #2803, #8545 ) ;
#13271=FACE_OUTER_BOUND ( 'NONE', #11694, .T. ) ;
#13280=AXIS2_PLACEMENT_3D ( 'NONE', #10354, #971, #5723 ) ;
#13284=AXIS2_PLACEMENT_3D ( 'NONE', #10863, #5127, #14571 ) ;
#13290=CARTESIAN_POINT ( 'NONE',  ( 16.18545172092247242, 11.99999970914575798, -0.4207436990616704175 ) ) ;
#13307=VECTOR ( 'NONE', #9542, 999.9999999999998863 ) ;
#13313=CYLINDRICAL_SURFACE ( 'NONE', #9424, 3.000000000000000888 ) ;
#13317=EDGE_CURVE ( 'NONE', #8152, #8702, #1065, .T. ) ;
#13333=DIRECTION ( 'NONE',  ( 0.9999934663667179313, -1.567696289299852222E-18, 0.003614861529252313445 ) ) ;
#13339=VECTOR ( 'NONE', #8776, 1000.000000000000114 ) ;
#13340=DIRECTION ( 'NONE',  ( -1.000000000000000000, -0.000000000000000000, -0.000000000000000000 ) ) ;
#13341=EDGE_CURVE ( 'NONE', #5823, #13360, #13086, .T. ) ;
#13351=CARTESIAN_POINT ( 'NONE',  ( 10.10406781373725771, -85.69524470659703752, 69.08979243323349806 ) ) ;
#13353=ADVANCED_FACE ( 'NONE', ( #1119 ), #3447, .T. ) ;
#13360=VERTEX_POINT ( 'NONE', #2508 ) ;
#13362=FACE_OUTER_BOUND ( 'NONE', #3016, .T. ) ;
#13376=ORIENTED_EDGE ( 'NONE', *, *, #6903, .F. ) ;
#13396=CARTESIAN_POINT ( 'NONE',  ( -12.81835358098578759, -12.00000029085424202, -0.3335879563140091153 ) ) ;
#13397=DIRECTION ( 'NONE',  ( -3.614007241618342978E-17, -1.000000000000000000, -0.000000000000000000 ) ) ;
#13398=DIRECTION ( 'NONE',  ( 0.9961946980917453232, -7.200509705930740925E-17, 0.08715574274766159368 ) ) ;
#13404=CARTESIAN_POINT ( 'NONE',  ( 17.18164641901421419, 3.654316742536407592, 0.2664120436859910845 ) ) ;
#13425=AXIS2_PLACEMENT_3D ( 'NONE', #4385, #13918, #6723 ) ;
#13426=EDGE_CURVE ( 'NONE', #12491, #6308, #10476, .T. ) ;
#13429=ORIENTED_EDGE ( 'NONE', *, *, #13799, .T. ) ;
#13430=VERTEX_POINT ( 'NONE', #9486 ) ;
#13437=DIRECTION ( 'NONE',  ( 0.000000000000000000, -1.000000000000000000, -4.336808689942017736E-16 ) ) ;
#13438=DIRECTION ( 'NONE',  ( 0.000000000000000000, 4.336808689942017736E-16, -1.000000000000000000 ) ) ;
#13449=CARTESIAN_POINT ( 'NONE',  ( 21.98164641901421135, -12.60000029085423812, -8.183940086454239093 ) ) ;
#13455=( GEOMETRIC_REPRESENTATION_CONTEXT ( 3 ) GLOBAL_UNCERTAINTY_ASSIGNED_CONTEXT ( ( #13531 ) ) GLOBAL_UNIT_ASSIGNED_CONTEXT ( ( #600, #6375, #3088 ) ) REPRESENTATION_CONTEXT ( 'NONE', 'WORKASPACE' ) );
#13459=CIRCLE ( 'NONE', #1303, 4.000000000000004441 ) ;
#13474=CARTESIAN_POINT ( 'NONE',  ( -13.41835358098579079, -11.75147215343038631, 0.2664120436859898633 ) ) ;
#13475=DIRECTION ( 'NONE',  ( -0.9961946980917452121, 3.779777825264100874E-17, -0.08715574274766163532 ) ) ;
#13481=CYLINDRICAL_SURFACE ( 'NONE', #4009, 1.000000000000001110 ) ;
#13486=DIRECTION ( 'NONE',  ( -0.9961946980917452121, 3.779777825264100874E-17, -0.08715574274766163532 ) ) ;
#13497=AXIS2_PLACEMENT_3D ( 'NONE', #14329, #7137, #14174 ) ;
#13503=ADVANCED_FACE ( 'NONE', ( #8486 ), #5003, .F. ) ;
#13515=DIRECTION ( 'NONE',  ( 0.000000000000000000, -1.000000000000000000, -4.336808689942017736E-16 ) ) ;
#13519=EDGE_CURVE ( 'NONE', #5033, #13053, #1507, .T. ) ;
#13520=CARTESIAN_POINT ( 'NONE',  ( -12.81835358098578403, 12.39999970914576188, -9.367156043074160721 ) ) ;
#13524=FACE_OUTER_BOUND ( 'NONE', #7639, .T. ) ;
#13530=CIRCLE ( 'NONE', #4362, 0.9999999999999994449 ) ;
#13531=UNCERTAINTY_MEASURE_WITH_UNIT (LENGTH_MEASURE( 1.000000000000000082E-05 ), #600, 'distance_accuracy_value', 'NONE');
#13544=DIRECTION ( 'NONE',  ( -1.258331998315348991E-39, 1.000000000000000000, 4.336808689942017243E-16 ) ) ;
#13547=DIRECTION ( 'NONE',  ( -1.000000000000000000, 0.000000000000000000, -0.000000000000000000 ) ) ;
#13549=DIRECTION ( 'NONE',  ( -1.000000000000000000, 0.000000000000000000, -0.000000000000000000 ) ) ;
#13560=LINE ( 'NONE', #2840, #60 ) ;
#13565=FACE_OUTER_BOUND ( 'NONE', #8784, .T. ) ;
#13571=CIRCLE ( 'NONE', #3396, 0.5999999999999998668 ) ;
#13573=DIRECTION ( 'NONE',  ( -0.9961946980917453232, 7.200509705930738460E-17, -0.08715574274766157981 ) ) ;
#13574=CYLINDRICAL_SURFACE ( 'NONE', #3317, 0.9999999999999994449 ) ;
#13576=CARTESIAN_POINT ( 'NONE',  ( 17.18164641901421419, 11.39999970914576011, 0.8664120436859875651 ) ) ;
#13585=ORIENTED_EDGE ( 'NONE', *, *, #13960, .F. ) ;
#13619=CARTESIAN_POINT ( 'NONE',  ( 21.98164641901421135, 11.99999970914576686, -14.73358795631400575 ) ) ;
#13629=DIRECTION ( 'NONE',  ( 0.000000000000000000, -1.000000000000000000, 0.000000000000000000 ) ) ;
#13641=LINE ( 'NONE', #4401, #12911 ) ;
#13644=CARTESIAN_POINT ( 'NONE',  ( 17.21739630941073429, -3.630123888347186245, 0.07286771090926238981 ) ) ;
#13661=LINE ( 'NONE', #6464, #7407 ) ;
#13667=EDGE_LOOP ( 'NONE', ( #4058, #5136, #11781, #1044 ) ) ;
#13671=EDGE_LOOP ( 'NONE', ( #2949, #688, #2444, #11182 ) ) ;
#13675=LINE ( 'NONE', #10322, #14667 ) ;
#13691=ORIENTED_EDGE ( 'NONE', *, *, #11256, .F. ) ;
#13693=ORIENTED_EDGE ( 'NONE', *, *, #9252, .T. ) ;
#13708=EDGE_CURVE ( 'NONE', #4222, #11928, #2425, .T. ) ;
#13713=ORIENTED_EDGE ( 'NONE', *, *, #12258, .T. ) ;
#13718=VECTOR ( 'NONE', #12426, 1000.000000000000000 ) ;
#13719=CARTESIAN_POINT ( 'NONE',  ( -13.41835358098578723, -2.908542394189813650E-07, 0.2664120436859911956 ) ) ;
#13721=DIRECTION ( 'NONE',  ( 0.000000000000000000, 1.000000000000000000, 4.336808689942017736E-16 ) ) ;
#13723=VERTEX_POINT ( 'NONE', #4682 ) ;
#13737=VECTOR ( 'NONE', #1690, 1000.000000000000114 ) ;
#13741=DIRECTION ( 'NONE',  ( -0.9961946980917452121, 3.779777825264100874E-17, -0.08715574274766163532 ) ) ;
#13752=CARTESIAN_POINT ( 'NONE',  ( -22.96690797774568082, 1.660051434983101380E-15, 52.36213013816526285 ) ) ;
#13762=CIRCLE ( 'NONE', #14491, 0.9999999999999994449 ) ;
#13789=ADVANCED_FACE ( 'NONE', ( #14208 ), #2343, .T. ) ;
#13795=PRESENTATION_STYLE_ASSIGNMENT (( #8751 ) ) ;
#13799=EDGE_CURVE ( 'NONE', #856, #11545, #10, .T. ) ;
#13805=ORIENTED_EDGE ( 'NONE', *, *, #10190, .T. ) ;
#13831=LINE ( 'NONE', #2030, #11556 ) ;
#13842=ORIENTED_EDGE ( 'NONE', *, *, #12853, .F. ) ;
#13844=ORIENTED_EDGE ( 'NONE', *, *, #7611, .F. ) ;
#13846=VECTOR ( 'NONE', #10840, 999.9999999999998863 ) ;
#13856=VERTEX_POINT ( 'NONE', #8695 ) ;
#13864=CARTESIAN_POINT ( 'NONE',  ( 1.592763020438999089, -1.151251418009690488E-16, 0.1393487079717274646 ) ) ;
#13869=ORIENTED_EDGE ( 'NONE', *, *, #7611, .T. ) ;
#13885=DIRECTION ( 'NONE',  ( -0.000000000000000000, -1.000000000000000000, -0.000000000000000000 ) ) ;
#13891=ORIENTED_EDGE ( 'NONE', *, *, #12541, .F. ) ;
#13897=EDGE_CURVE ( 'NONE', #2678, #14347, #480, .T. ) ;
#13918=DIRECTION ( 'NONE',  ( -0.9961946980917452121, 3.779777825264100874E-17, -0.08715574274766163532 ) ) ;
#13923=CARTESIAN_POINT ( 'NONE',  ( -4.486254801108944257, 11.99999970914572778, 69.62284035768031742 ) ) ;
#13935=DIRECTION ( 'NONE',  ( 0.000000000000000000, 0.000000000000000000, -1.000000000000000000 ) ) ;
#13937=CARTESIAN_POINT ( 'NONE',  ( 17.18164641901421419, 11.39999970914576011, 0.8664120436859875651 ) ) ;
#13940=ORIENTED_EDGE ( 'NONE', *, *, #6253, .T. ) ;
#13941=DIRECTION ( 'NONE',  ( 0.000000000000000000, 0.9860132971832695770, 0.1666666666666655749 ) ) ;
#13944=EDGE_LOOP ( 'NONE', ( #2700, #709, #591, #7028, #7309, #7408, #468, #14517, #13844, #7899, #15309, #1464, #5189, #685 ) ) ;
#13960=EDGE_CURVE ( 'NONE', #7132, #11742, #9624, .T. ) ;
#13968=ORIENTED_EDGE ( 'NONE', *, *, #8879, .F. ) ;
#13969=DIRECTION ( 'NONE',  ( 0.9961946980917452121, 0.000000000000000000, 0.08715574274766160756 ) ) ;
#13970=AXIS2_PLACEMENT_3D ( 'NONE', #9695, #5286, #2793 ) ;
#13974=ADVANCED_FACE ( 'NONE', ( #2654, #1562, #6318 ), #4982, .T. ) ;
#13984=CIRCLE ( 'NONE', #5830, 0.5999999999999998668 ) ;
#13990=EDGE_LOOP ( 'NONE', ( #7993, #6848, #10298, #2040 ) ) ;
#14004=DIRECTION ( 'NONE',  ( 0.9999934663667180423, -0.000000000000000000, 0.003614861529253208996 ) ) ;
#14029=EDGE_LOOP ( 'NONE', ( #1500, #13940, #4806, #4302, #13429, #3299 ) ) ;
#14037=ADVANCED_FACE ( 'NONE', ( #13362 ), #6233, .T. ) ;
#14042=LINE ( 'NONE', #9449, #13011 ) ;
#14055=CIRCLE ( 'NONE', #11575, 1.199999999999999734 ) ;
#14057=CARTESIAN_POINT ( 'NONE',  ( 21.98164641901421135, -12.00000029085423670, -14.13358795631400611 ) ) ;
#14059=EDGE_CURVE ( 'NONE', #12175, #3871, #12180, .T. ) ;
#14066=CARTESIAN_POINT ( 'NONE',  ( 22.58164641901421632, -2.908542394189813650E-07, -0.3335879563140091153 ) ) ;
#14071=VERTEX_POINT ( 'NONE', #10942 ) ;
#14073=ORIENTED_EDGE ( 'NONE', *, *, #3751, .F. ) ;
#14076=DIRECTION ( 'NONE',  ( 0.000000000000000000, 1.000000000000000000, 0.000000000000000000 ) ) ;
#14082=CARTESIAN_POINT ( 'NONE',  ( 17.23697745638123280, -3.654316742536412033, -0.03314156585704672309 ) ) ;
#14088=AXIS2_PLACEMENT_3D ( 'NONE', #1619, #9753, #1472 ) ;
#14096=DIRECTION ( 'NONE',  ( 1.000000000000000000, 0.000000000000000000, 0.000000000000000000 ) ) ;
#14104=ORIENTED_EDGE ( 'NONE', *, *, #9680, .F. ) ;
#14115=CARTESIAN_POINT ( 'NONE',  ( 1.581646419014216542, -11.40000029085424238, 0.2664120436859911956 ) ) ;
#14123=EDGE_LOOP ( 'NONE', ( #7213, #12196, #10469, #8370, #6001 ) ) ;
#14135=EDGE_CURVE ( 'NONE', #3706, #8660, #11555, .T. ) ;
#14136=EDGE_LOOP ( 'NONE', ( #9895, #12654, #2227, #14606 ) ) ;
#14153=AXIS2_PLACEMENT_3D ( 'NONE', #8253, #8412, #11829 ) ;
#14164=FACE_OUTER_BOUND ( 'NONE', #14029, .T. ) ;
#14174=DIRECTION ( 'NONE',  ( 0.000000000000000000, 1.000000000000000000, 0.000000000000000000 ) ) ;
#14175=EDGE_CURVE ( 'NONE', #1550, #4558, #8772, .T. ) ;
#14178=ORIENTED_EDGE ( 'NONE', *, *, #1933, .T. ) ;
#14180=VECTOR ( 'NONE', #3270, 1000.000000000000000 ) ;
#14199=CARTESIAN_POINT ( 'NONE',  ( 22.28931995216796835, 10.99999970914572778, 69.13384072020835447 ) ) ;
#14208=FACE_OUTER_BOUND ( 'NONE', #8929, .T. ) ;
#14210=LINE ( 'NONE', #14293, #6119 ) ;
#14225=CIRCLE ( 'NONE', #1845, 0.6000000000000000888 ) ;
#14249=CARTESIAN_POINT ( 'NONE',  ( 21.98164641901421135, 11.99999970914575798, -0.3335879563140091153 ) ) ;
#14251=ORIENTED_EDGE ( 'NONE', *, *, #22, .F. ) ;
#14263=CARTESIAN_POINT ( 'NONE',  ( -4.522482571421200248, -11.00000029085428110, 70.03692566716176771 ) ) ;
#14287=DIRECTION ( 'NONE',  ( 0.000000000000000000, 4.336808689942017736E-16, -1.000000000000000000 ) ) ;
#14293=CARTESIAN_POINT ( 'NONE',  ( 22.58164641901421632, 5.075009326258863140, -11.09921666827752951 ) ) ;
#14306=CARTESIAN_POINT ( 'NONE',  ( -13.41835358098578723, -12.60000029085423812, -8.183940086454239093 ) ) ;
#14311=CARTESIAN_POINT ( 'NONE',  ( 17.00399103715874460, 11.48932363952878788, 0.2918479299858876552 ) ) ;
#14329=CARTESIAN_POINT ( 'NONE',  ( -12.81835358098578759, -11.40000029085423705, -11.73358795631401463 ) ) ;
#14347=VERTEX_POINT ( 'NONE', #9904 ) ;
#14350=CARTESIAN_POINT ( 'NONE',  ( 23.77513017582411692, -1.718469852516944459E-15, 56.45152858669899132 ) ) ;
#14355=FACE_OUTER_BOUND ( 'NONE', #14457, .T. ) ;
#14378=CYLINDRICAL_SURFACE ( 'NONE', #4634, 0.6000000000000000888 ) ;
#14384=DIRECTION ( 'NONE',  ( -0.08715574274766157981, 1.084202172485503818E-16, 0.9961946980917452121 ) ) ;
#14385=TOROIDAL_SURFACE ( 'NONE', #7950, 1.200000000000000178, 0.6000000000000000888 ) ;
#14386=DIRECTION ( 'NONE',  ( -1.000000000000000000, 0.000000000000000000, 0.000000000000000000 ) ) ;
#14388=CARTESIAN_POINT ( 'NONE',  ( 0.000000000000000000, 1.507583120841093915E-15, -56.77834603255778489 ) ) ;
#14390=ORIENTED_EDGE ( 'NONE', *, *, #11612, .F. ) ;
#14393=ORIENTED_EDGE ( 'NONE', *, *, #9335, .T. ) ;
#14425=EDGE_CURVE ( 'NONE', #9494, #8700, #11927, .T. ) ;
#14427=DIRECTION ( 'NONE',  ( 0.1816390095645149805, 0.000000000000000000, -0.9833652781161342782 ) ) ;
#14439=CIRCLE ( 'NONE', #321, 1.199999999999711520 ) ;
#14447=AXIS2_PLACEMENT_3D ( 'NONE', #13449, #11339, #7559 ) ;
#14448=CARTESIAN_POINT ( 'NONE',  ( -3.127990687458614971, 2.260916199238037239E-16, 54.09781049769389938 ) ) ;
#14457=EDGE_LOOP ( 'NONE', ( #1240, #14178, #895, #3900, #1573, #13693, #752, #8973, #5454 ) ) ;
#14458=DIRECTION ( 'NONE',  ( 1.000000000000000000, 0.000000000000000000, 0.000000000000000000 ) ) ;
#14471=LINE ( 'NONE', #6274, #3369 ) ;
#14473=PLANE ( 'NONE',  #104 ) ;
#14476=DIRECTION ( 'NONE',  ( 1.000000000000000000, 0.000000000000000000, 0.000000000000000000 ) ) ;
#14483=ORIENTED_EDGE ( 'NONE', *, *, #8021, .T. ) ;
#14491=AXIS2_PLACEMENT_3D ( 'NONE', #1330, #10482, #15209 ) ;
#14496=ORIENTED_EDGE ( 'NONE', *, *, #10278, .T. ) ;
#14506=PLANE ( 'NONE',  #1043 ) ;
#14516=DIRECTION ( 'NONE',  ( 0.000000000000000000, 0.000000000000000000, -1.000000000000000000 ) ) ;
#14517=ORIENTED_EDGE ( 'NONE', *, *, #1838, .T. ) ;
#14521=CARTESIAN_POINT ( 'NONE',  ( 11.10026251182900481, -85.69524470659703752, 69.17694817598116686 ) ) ;
#14526=CARTESIAN_POINT ( 'NONE',  ( 21.98164641901421135, -11.40000029085424238, -0.3335879563140091153 ) ) ;
#14529=DIRECTION ( 'NONE',  ( 1.000000000000000000, -0.000000000000000000, 0.000000000000000000 ) ) ;
#14532=ORIENTED_EDGE ( 'NONE', *, *, #3335, .F. ) ;
#14562=ORIENTED_EDGE ( 'NONE', *, *, #14640, .T. ) ;
#14563=ORIENTED_EDGE ( 'NONE', *, *, #13059, .F. ) ;
#14564=EDGE_CURVE ( 'NONE', #6473, #5823, #13641, .T. ) ;
#14569=AXIS2_PLACEMENT_3D ( 'NONE', #15108, #13741, #10456 ) ;
#14571=DIRECTION ( 'NONE',  ( 0.000000000000000000, 0.000000000000000000, -1.000000000000000000 ) ) ;
#14574=PLANE ( 'NONE',  #8262 ) ;
#14577=ORIENTED_EDGE ( 'NONE', *, *, #6805, .T. ) ;
#14603=DIRECTION ( 'NONE',  ( 0.9961946980917452121, -3.779777825264101491E-17, 0.08715574274766160756 ) ) ;
#14606=ORIENTED_EDGE ( 'NONE', *, *, #13014, .T. ) ;
#14609=ORIENTED_EDGE ( 'NONE', *, *, #4778, .F. ) ;
#14614=CARTESIAN_POINT ( 'NONE',  ( 15.14695642955105193, -1.094824204497501265E-15, 22.92302504315390621 ) ) ;
#14632=AXIS2_PLACEMENT_3D ( 'NONE', #7027, #13547, #257 ) ;
#14640=EDGE_CURVE ( 'NONE', #11342, #1533, #7199, .T. ) ;
#14641=CARTESIAN_POINT ( 'NONE',  ( 22.58164641901421632, 11.99999970914576330, -11.73358795631400753 ) ) ;
#14651=AXIS2_PLACEMENT_3D ( 'NONE', #12991, #4845, #11896 ) ;
#14667=VECTOR ( 'NONE', #9232, 999.9999999999998863 ) ;
#14694=CARTESIAN_POINT ( 'NONE',  ( -6.714472293954755422, -12.00000029085427578, 37.72291661448763733 ) ) ;
#14702=VECTOR ( 'NONE', #1121, 1000.000000000000000 ) ;
#14725=VERTEX_POINT ( 'NONE', #11589 ) ;
#14743=PRODUCT_DEFINITION_SHAPE ( 'NONE', 'NONE',  #5538 ) ;
#14750=VERTEX_POINT ( 'NONE', #3138 ) ;
#14763=CARTESIAN_POINT ( 'NONE',  ( 22.58164641901421632, -12.00000029085423670, -11.73358795631401463 ) ) ;
#14773=ORIENTED_EDGE ( 'NONE', *, *, #13897, .T. ) ;
#14775=FACE_OUTER_BOUND ( 'NONE', #5387, .T. ) ;
#14777=FACE_OUTER_BOUND ( 'NONE', #1931, .T. ) ;
#14787=VERTEX_POINT ( 'NONE', #7873 ) ;
#14788=CIRCLE ( 'NONE', #8108, 0.5999999999999998668 ) ;
#14817=CARTESIAN_POINT ( 'NONE',  ( 17.18164641901421419, -2.908542394189813650E-07, 0.2664120436859911956 ) ) ;
#14820=EDGE_CURVE ( 'NONE', #6505, #12175, #3599, .T. ) ;
#14840=ADVANCED_FACE ( 'NONE', ( #3513 ), #9634, .F. ) ;
#14847=EDGE_CURVE ( 'NONE', #4158, #4974, #7728, .T. ) ;
#14853=DIRECTION ( 'NONE',  ( 1.000000000000000000, 0.000000000000000000, 0.000000000000000000 ) ) ;
#14868=VERTEX_POINT ( 'NONE', #12057 ) ;
#14879=DIRECTION ( 'NONE',  ( 0.000000000000000000, 1.000000000000000000, 0.000000000000000000 ) ) ;
#14884=AXIS2_PLACEMENT_3D ( 'NONE', #3910, #8938, #333 ) ;
#14896=LINE ( 'NONE', #4285, #159 ) ;
#14904=ORIENTED_EDGE ( 'NONE', *, *, #4615, .T. ) ;
#14922=CARTESIAN_POINT ( 'NONE',  ( 21.98164641901421135, -2.908542394189813650E-07, 0.2664120436859911956 ) ) ;
#14926=AXIS2_PLACEMENT_3D ( 'NONE', #10536, #2008, #12798 ) ;
#14937=CARTESIAN_POINT ( 'NONE',  ( 17.12895037488186389, -3.654606557864051197, 0.2687305842673423095 ) ) ;
#14951=VERTEX_POINT ( 'NONE', #1428 ) ;
#14954=FACE_OUTER_BOUND ( 'NONE', #13667, .T. ) ;
#14974=DIRECTION ( 'NONE',  ( 0.000000000000000000, -4.336808689942017736E-16, 1.000000000000000000 ) ) ;
#15003=ORIENTED_EDGE ( 'NONE', *, *, #4556, .T. ) ;
#15016=FILL_AREA_STYLE ('',( #12936 ) ) ;
#15021=DIRECTION ( 'NONE',  ( 1.000000000000000000, 0.000000000000000000, 0.000000000000000000 ) ) ;
#15042=LINE ( 'NONE', #6628, #13718 ) ;
#15044=CARTESIAN_POINT ( 'NONE',  ( -2.779367716467973093, 7.159503395827459929E-16, 50.11303170532690388 ) ) ;
#15071=EDGE_CURVE ( 'NONE', #5823, #4668, #10424, .T. ) ;
#15099=ORIENTED_EDGE ( 'NONE', *, *, #9718, .T. ) ;
#15106=EDGE_CURVE ( 'NONE', #14347, #13430, #9788, .T. ) ;
#15107=EDGE_CURVE ( 'NONE', #8660, #9779, #7710, .T. ) ;
#15108=CARTESIAN_POINT ( 'NONE',  ( -0.2824495906440828152, 2.041549731959705837E-17, 21.57312693144813665 ) ) ;
#15116=ADVANCED_FACE ( 'NONE', ( #7486 ), #6332, .F. ) ;
#15124=LINE ( 'NONE', #9237, #14180 ) ;
#15129=DIRECTION ( 'NONE',  ( -0.9961946980917453232, 7.200509705930738460E-17, -0.08715574274766157981 ) ) ;
#15132=DIRECTION ( 'NONE',  ( -0.9961946980917452121, 7.200509705930738460E-17, -0.08715574274766156593 ) ) ;
#15150=CARTESIAN_POINT ( 'NONE',  ( 17.18164641901421419, -3.654316742536411589, 0.2664120436859910845 ) ) ;
#15160=CIRCLE ( 'NONE', #14926, 0.9999999999999956701 ) ;
#15161=CARTESIAN_POINT ( 'NONE',  ( -8.108964177917338034, 5.861171052203404620E-16, 53.66203178395558382 ) ) ;
#15166=VERTEX_POINT ( 'NONE', #4587 ) ;
#15177=VECTOR ( 'NONE', #8701, 1000.000000000000000 ) ;
#15182=( BOUNDED_CURVE ( )  B_SPLINE_CURVE ( 3, ( #12724, #5834, #1080, #1946 ),
 .UNSPECIFIED., .F., .T. ) 
 B_SPLINE_CURVE_WITH_KNOTS ( ( 4, 4 ),
 ( 6.195245264107405170, 6.283185307179586232 ),
 .UNSPECIFIED. ) 
 CURVE ( )  GEOMETRIC_REPRESENTATION_ITEM ( )  RATIONAL_B_SPLINE_CURVE ( ( 1.000000000000000000, 0.9993556495590054656, 0.9993556495590054656, 1.000000000000000000 ) ) 
 REPRESENTATION_ITEM ( '' )  );
#15200=EDGE_CURVE ( 'NONE', #11747, #6469, #13675, .T. ) ;
#15209=DIRECTION ( 'NONE',  ( 0.9961946980917453232, -8.673617379884040205E-15, 0.08715574274766051122 ) ) ;
#15215=ADVANCED_FACE ( 'NONE', ( #10393 ), #11412, .F. ) ;
#15224=FACE_OUTER_BOUND ( 'NONE', #14136, .T. ) ;
#15238=AXIS2_PLACEMENT_3D ( 'NONE', #1622, #11311, #12562 ) ;
#15242=CARTESIAN_POINT ( 'NONE',  ( -12.81835358098578403, 11.99999970914576330, -11.73358795631400753 ) ) ;
#15245=DIRECTION ( 'NONE',  ( -0.08715574274766155205, 0.000000000000000000, 0.9961946980917452121 ) ) ;
#15254=VECTOR ( 'NONE', #6280, 1000.000000000000000 ) ;
#15268=CARTESIAN_POINT ( 'NONE',  ( 22.58164641901421632, 11.99999970914575798, -0.3335879563140091153 ) ) ;
#15276=ORIENTED_EDGE ( 'NONE', *, *, #11326, .F. ) ;
#15277=EDGE_LOOP ( 'NONE', ( #2767, #367, #13376, #10788 ) ) ;
#15279=AXIS2_PLACEMENT_3D ( 'NONE', #3435, #2041, #10485 ) ;
#15303=ADVANCED_FACE ( 'NONE', ( #5929 ), #10874, .F. ) ;
#15307=LINE ( 'NONE', #14082, #9495 ) ;
#15308=ADVANCED_FACE ( 'NONE', ( #6167 ), #7159, .T. ) ;
#15309=ORIENTED_EDGE ( 'NONE', *, *, #10666, .T. ) ;
#15320=CIRCLE ( 'NONE', #6923, 0.5999999999999998668 ) ;
#15322=SURFACE_STYLE_FILL_AREA ( #15016 ) ;
#15323=CARTESIAN_POINT ( 'NONE',  ( -1.733498803496028140, -12.00000029085427578, 38.15869532822594579 ) ) ;
#15328=VERTEX_POINT ( 'NONE', #4825 ) ;
ENDSEC;
END-ISO-10303-21;
